ISO-10303-21;
HEADER;
FILE_DESCRIPTION (('STEP AP214'),
    '1' );
FILE_NAME ('torque nut 09_iso_ISO 10512-M12x1.5-N.step',
    '2026-10-23T20:35:44',
    ( '' ),
    ( '' ),
    'SwSTEP 2.0',
    'SolidWorks 2025',
    '' );
FILE_SCHEMA (( 'AUTOMOTIVE_DESIGN' ));
ENDSEC;

DATA;
#1=VERTEX_POINT ( 'NONE', #349 ) ;
#6=CARTESIAN_POINT ( 'NONE',  ( -0.3543307086614173596, -0.1713008003332314455, -0.02204270589528184790 ) ) ;
#11=DIRECTION ( 'NONE',  ( -0.000000000000000000, -0.000000000000000000, 1.000000000000000000 ) ) ;
#19=FACE_OUTER_BOUND ( 'NONE', #4746, .T. ) ;
#24=CIRCLE ( 'NONE', #5042, 0.2362204724409449619 ) ;
#31=CARTESIAN_POINT ( 'NONE',  ( 0.3543307086614173596, -0.2045729300278204543, -0.03164754241312491001 ) ) ;
#37=ORIENTED_EDGE ( 'NONE', *, *, #488, .F. ) ;
#40=DIRECTION ( 'NONE',  ( 1.000000000000000000, 0.000000000000000000, 0.000000000000000000 ) ) ;
#62=CARTESIAN_POINT ( 'NONE',  ( 0.000000000000000000, 0.000000000000000000, 0.000000000000000000 ) ) ;
#80=ORIENTED_EDGE ( 'NONE', *, *, #4669, .F. ) ;
#88=CARTESIAN_POINT ( 'NONE',  ( 0.000000000000000000, 0.000000000000000000, -0.4082677165354330340 ) ) ;
#92=ORIENTED_EDGE ( 'NONE', *, *, #6917, .F. ) ;
#94=B_SPLINE_CURVE_WITH_KNOTS ( 'NONE', 3,
 ( #4855, #1250, #5355, #240, #5937, #4783, #5402, #7182 ),
 .UNSPECIFIED., .F., .F.,
 ( 4, 2, 2, 4 ),
 ( 0.005257893453559878486, 0.006567392922673220834, 0.007876892391786563183, 0.01049589133001324615 ),
 .UNSPECIFIED. ) ;
#123=LINE ( 'NONE', #695, #2284 ) ;
#131=CARTESIAN_POINT ( 'NONE',  ( 0.3543307086614173040, 0.2045729300278205931, -0.3766201741223081378 ) ) ;
#132=ORIENTED_EDGE ( 'NONE', *, *, #2423, .T. ) ;
#148=EDGE_CURVE ( 'NONE', #5183, #4410, #5219, .T. ) ;
#150=CARTESIAN_POINT ( 'NONE',  ( 0.3543307086614173040, -0.06891495372886455306, -0.002971448422589516563 ) ) ;
#153=DIRECTION ( 'NONE',  ( -0.000000000000000000, -0.000000000000000000, 1.000000000000000000 ) ) ;
#164=CIRCLE ( 'NONE', #5660, 0.2362204724409449619 ) ;
#166=AXIS2_PLACEMENT_3D ( 'NONE', #1159, #469, #4589 ) ;
#171=DIRECTION ( 'NONE',  ( 0.000000000000000000, -0.000000000000000000, 1.000000000000000000 ) ) ;
#182=ORIENTED_EDGE ( 'NONE', *, *, #5478, .F. ) ;
#197=DIRECTION ( 'NONE',  ( -0.000000000000000000, -0.000000000000000000, 1.000000000000000000 ) ) ;
#199=ORIENTED_EDGE ( 'NONE', *, *, #4211, .F. ) ;
#224=UNCERTAINTY_MEASURE_WITH_UNIT (LENGTH_MEASURE( 1.000000000000000082E-05 ), #1420, 'distance_accuracy_value', 'NONE');
#226=FACE_BOUND ( 'NONE', #2302, .T. ) ;
#233=FACE_OUTER_BOUND ( 'NONE', #3715, .T. ) ;
#235=CARTESIAN_POINT ( 'NONE',  ( 0.3543307086614173596, -0.2045729300278204543, -0.3766201741223081378 ) ) ;
#238=ORIENTED_EDGE ( 'NONE', *, *, #6320, .T. ) ;
#240=CARTESIAN_POINT ( 'NONE',  ( 0.1171503679538647841, -0.3415090635818134879, -0.003642820150508935782 ) ) ;
#247=ORIENTED_EDGE ( 'NONE', *, *, #6320, .F. ) ;
#259=CARTESIAN_POINT ( 'NONE',  ( 0.3543307086614173040, 0.2045729300278199825, -0.4082677165354330340 ) ) ;
#261=DIRECTION ( 'NONE',  ( -0.000000000000000000, 0.000000000000000000, -1.000000000000000000 ) ) ;
#273=ORIENTED_EDGE ( 'NONE', *, *, #1681, .F. ) ;
#288=CARTESIAN_POINT ( 'NONE',  ( 0.000000000000000000, 0.000000000000000000, 0.000000000000000000 ) ) ;
#290=CARTESIAN_POINT ( 'NONE',  ( -0.1771653543307088186, -0.3068593950417299876, 7.886165872636028972E-17 ) ) ;
#292=LINE ( 'NONE', #4459, #6747 ) ;
#300=PLANE ( 'NONE',  #6109 ) ;
#305=CLOSED_SHELL ( 'NONE', ( #1149, #6868, #3499, #5163, #6222, #1636, #5575, #2053, #3601, #534, #3181, #4486, #5802, #2374, #6509, #6038, #2797, #4111, #3420, #2152, #3035, #947, #2811, #6077, #4630, #5716, #6046, #5573, #7144, #802, #7479, #5229, #6436 ) ) ;
#328=ORIENTED_EDGE ( 'NONE', *, *, #2423, .F. ) ;
#336=DIRECTION ( 'NONE',  ( -0.8660254037844382635, 0.5000000000000006661, 0.000000000000000000 ) ) ;
#340=EDGE_CURVE ( 'NONE', #1419, #4225, #5767, .T. ) ;
#343=FACE_OUTER_BOUND ( 'NONE', #5945, .T. ) ;
#348=ORIENTED_EDGE ( 'NONE', *, *, #6732, .T. ) ;
#349=CARTESIAN_POINT ( 'NONE',  ( -0.1771653543307089573, 0.3068593950417301541, -0.4082677165354330340 ) ) ;
#357=EDGE_LOOP ( 'NONE', ( #3994, #2629, #763 ) ) ;
#374=CARTESIAN_POINT ( 'NONE',  ( 0.05817553349160906745, 0.3755582001340100340, -0.3942397458900142593 ) ) ;
#392=CARTESIAN_POINT ( 'NONE',  ( 0.000000000000000000, 0.000000000000000000, 0.1188976377952756375 ) ) ;
#395=ORIENTED_EDGE ( 'NONE', *, *, #1081, .F. ) ;
#399=MECHANICAL_DESIGN_GEOMETRIC_PRESENTATION_REPRESENTATION('',(#7343),#5389);
#404=ORIENTED_EDGE ( 'NONE', *, *, #5065, .F. ) ;
#405=CARTESIAN_POINT ( 'NONE',  ( -0.3543307086614173040, 0.000000000000000000, -0.4082677165354330340 ) ) ;
#406=ORIENTED_EDGE ( 'NONE', *, *, #5878, .F. ) ;
#410=DIRECTION ( 'NONE',  ( -0.000000000000000000, -0.000000000000000000, 1.000000000000000000 ) ) ;
#418=CARTESIAN_POINT ( 'NONE',  ( 0.000000000000000000, 0.000000000000000000, 0.000000000000000000 ) ) ;
#430=CARTESIAN_POINT ( 'NONE',  ( 0.000000000000000000, 0.2066929133858267931, 0.1188976377952756375 ) ) ;
#433=CARTESIAN_POINT ( 'NONE',  ( 0.3543307086614173040, 0.2045729300278205931, -0.03164754241312491001 ) ) ;
#449=CARTESIAN_POINT ( 'NONE',  ( -0.2520187439128739326, -0.2636427704167116359, -0.4024809188492813328 ) ) ;
#469=DIRECTION ( 'NONE',  ( 0.000000000000000000, -0.000000000000000000, 1.000000000000000000 ) ) ;
#475=ORIENTED_EDGE ( 'NONE', *, *, #2364, .T. ) ;
#488=EDGE_CURVE ( 'NONE', #4739, #1108, #3971, .T. ) ;
#493=VECTOR ( 'NONE', #4622, 39.37007874015748143 ) ;
#497=CARTESIAN_POINT ( 'NONE',  ( -0.1470270249832137943, 0.3242597676034320586, -0.4075196867561205472 ) ) ;
#498=B_SPLINE_CURVE_WITH_KNOTS ( 'NONE', 3,
 ( #801, #3127, #3279, #3396, #6338, #6232, #6305, #2138 ),
 .UNSPECIFIED., .F., .F.,
 ( 4, 2, 2, 4 ),
 ( 0.005257893453559879353, 0.006567392922673220834, 0.007876892391786561448, 0.01049589133001324961 ),
 .UNSPECIFIED. ) ;
#500=CARTESIAN_POINT ( 'NONE',  ( -0.3543307086614173040, 0.000000000000000000, -0.4082677165354330340 ) ) ;
#516=ORIENTED_EDGE ( 'NONE', *, *, #4216, .T. ) ;
#522=VECTOR ( 'NONE', #4279, 39.37007874015748143 ) ;
#523=DIRECTION ( 'NONE',  ( 1.000000000000000000, 0.000000000000000000, 0.000000000000000000 ) ) ;
#528=CARTESIAN_POINT ( 'NONE',  ( 0.3543307086614172485, 0.000000000000000000, 7.886165872636028972E-17 ) ) ;
#532=DIRECTION ( 'NONE',  ( 0.000000000000000000, 0.000000000000000000, 1.000000000000000000 ) ) ;
#534=ADVANCED_FACE ( 'NONE', ( #2338 ), #7464, .F. ) ;
#541=CARTESIAN_POINT ( 'NONE',  ( 0.3543307086614173040, 0.2045729300278205931, -0.3766201741223081378 ) ) ;
#554=ORIENTED_EDGE ( 'NONE', *, *, #5878, .T. ) ;
#558=PRODUCT_DEFINITION ( 'UNKNOWN', '', #6558, #2961 ) ;
#562=EDGE_CURVE ( 'NONE', #4139, #6455, #5693, .T. ) ;
#587=LINE ( 'NONE', #2905, #4789 ) ;
#594=AXIS2_PLACEMENT_3D ( 'NONE', #7139, #4240, #4775 ) ;
#596=FACE_OUTER_BOUND ( 'NONE', #6777, .T. ) ;
#600=CARTESIAN_POINT ( 'NONE',  ( 0.000000000000000000, 0.000000000000000000, -0.4072677165354330331 ) ) ;
#601=AXIS2_PLACEMENT_3D ( 'NONE', #3839, #2758, #6170 ) ;
#611=CARTESIAN_POINT ( 'NONE',  ( 0.000000000000000000, 0.000000000000000000, -0.4082677165354330340 ) ) ;
#618=DIRECTION ( 'NONE',  ( 0.000000000000000000, -0.000000000000000000, 1.000000000000000000 ) ) ;
#621=CIRCLE ( 'NONE', #4896, 0.2066929133858267931 ) ;
#622=DIRECTION ( 'NONE',  ( 0.8660254037844382635, 0.5000000000000006661, 0.000000000000000000 ) ) ;
#636=DIRECTION ( 'NONE',  ( -0.000000000000000000, 0.000000000000000000, -1.000000000000000000 ) ) ;
#657=CARTESIAN_POINT ( 'NONE',  ( 0.000000000000000000, 0.000000000000000000, -0.4082677165354330340 ) ) ;
#659=CARTESIAN_POINT ( 'NONE',  ( -0.3543307086614173040, -0.06891495372886451143, -0.002971448422589511792 ) ) ;
#662=VERTEX_POINT ( 'NONE', #528 ) ;
#665=FACE_OUTER_BOUND ( 'NONE', #3589, .T. ) ;
#669=AXIS2_PLACEMENT_3D ( 'NONE', #1109, #7038, #4096 ) ;
#672=DIRECTION ( 'NONE',  ( -0.000000000000000000, -0.000000000000000000, 1.000000000000000000 ) ) ;
#681=CARTESIAN_POINT ( 'NONE',  ( -0.05817553349160984461, -0.3755582001340100895, -0.3942397458900140927 ) ) ;
#682=CARTESIAN_POINT ( 'NONE',  ( 0.3543307086614173040, -0.1372236123666514263, -0.01398679180475823416 ) ) ;
#685=FACE_OUTER_BOUND ( 'NONE', #2421, .T. ) ;
#691=FACE_OUTER_BOUND ( 'NONE', #2067, .T. ) ;
#695=CARTESIAN_POINT ( 'NONE',  ( 0.3543307086614173040, -0.2045729300278205376, -0.4082677165354330340 ) ) ;
#701=EDGE_CURVE ( 'NONE', #3513, #6455, #587, .T. ) ;
#717=CARTESIAN_POINT ( 'NONE',  ( -0.1771653543307089018, -0.3068593950417300986, -0.4082677165354330340 ) ) ;
#724=CARTESIAN_POINT ( 'NONE',  ( 0.3543307086614173040, -0.1372236123666513430, -0.3942809247306748865 ) ) ;
#763=ORIENTED_EDGE ( 'NONE', *, *, #1199, .T. ) ;
#770=AXIS2_PLACEMENT_3D ( 'NONE', #6990, #1284, #6503 ) ;
#778=DIRECTION ( 'NONE',  ( -1.000000000000000000, 0.000000000000000000, 0.000000000000000000 ) ) ;
#784=CARTESIAN_POINT ( 'NONE',  ( 0.000000000000000000, 0.000000000000000000, 0.000000000000000000 ) ) ;
#791=DIRECTION ( 'NONE',  ( 1.000000000000000000, 0.000000000000000000, 0.000000000000000000 ) ) ;
#801=CARTESIAN_POINT ( 'NONE',  ( 0.1771653543307089296, -0.3068593950417301541, -0.4082677165354330340 ) ) ;
#802=ADVANCED_FACE ( 'NONE', ( #665 ), #2984, .F. ) ;
#819=ORIENTED_EDGE ( 'NONE', *, *, #5100, .F. ) ;
#823=ORIENTED_EDGE ( 'NONE', *, *, #2569, .F. ) ;
#851=EDGE_CURVE ( 'NONE', #7286, #3362, #1476, .T. ) ;
#856=CARTESIAN_POINT ( 'NONE',  ( 0.000000000000000000, 0.000000000000000000, 0.1188976377952756375 ) ) ;
#860=ORIENTED_EDGE ( 'NONE', *, *, #6926, .T. ) ;
#884=ORIENTED_EDGE ( 'NONE', *, *, #2364, .F. ) ;
#889=AXIS2_PLACEMENT_3D ( 'NONE', #5715, #3333, #2261 ) ;
#892=CARTESIAN_POINT ( 'NONE',  ( 0.3543307086614173596, -0.2045729300278204543, -0.03164754241312491001 ) ) ;
#898=CIRCLE ( 'NONE', #5179, 0.3543307086614173596 ) ;
#907=AXIS2_PLACEMENT_3D ( 'NONE', #6219, #3810, #4309 ) ;
#929=VERTEX_POINT ( 'NONE', #3762 ) ;
#934=ORIENTED_EDGE ( 'NONE', *, *, #5286, .F. ) ;
#946=EDGE_CURVE ( 'NONE', #1068, #3331, #4296, .T. ) ;
#947=ADVANCED_FACE ( 'NONE', ( #2325 ), #1113, .T. ) ;
#959=CARTESIAN_POINT ( 'NONE',  ( 0.2073036836782038983, 0.2894590224800283051, -0.0007480297793123734124 ) ) ;
#967=FACE_OUTER_BOUND ( 'NONE', #3872, .T. ) ;
#969=ORIENTED_EDGE ( 'NONE', *, *, #562, .T. ) ;
#975=AXIS2_PLACEMENT_3D ( 'NONE', #1889, #3025, #4673 ) ;
#979=EDGE_CURVE ( 'NONE', #2951, #5183, #1377, .T. ) ;
#1000=VERTEX_POINT ( 'NONE', #2795 ) ;
#1014=DIRECTION ( 'NONE',  ( -1.000000000000000000, 1.224646799147353700E-16, 0.000000000000000000 ) ) ;
#1047=EDGE_LOOP ( 'NONE', ( #1242, #1268, #6541, #3497 ) ) ;
#1048=CARTESIAN_POINT ( 'NONE',  ( 0.000000000000000000, 0.000000000000000000, 0.1188976377952756375 ) ) ;
#1055=CARTESIAN_POINT ( 'NONE',  ( -0.3543307086614173040, 0.06965032677943189254, -0.003053646640237103489 ) ) ;
#1057=CARTESIAN_POINT ( 'NONE',  ( -0.2066929133858267931, 2.531258147843938473E-17, -0.4082677165354330340 ) ) ;
#1061=CIRCLE ( 'NONE', #5339, 0.2066929133858267931 ) ;
#1062=CARTESIAN_POINT ( 'NONE',  ( 0.3254211578371890567, 0.2212638669783392742, -0.02201102547170719764 ) ) ;
#1066=CARTESIAN_POINT ( 'NONE',  ( 0.1771653543307089296, 0.3068593950417301541, -0.4082677165354330340 ) ) ;
#1068=VERTEX_POINT ( 'NONE', #1784 ) ;
#1070=ORIENTED_EDGE ( 'NONE', *, *, #6917, .T. ) ;
#1081=EDGE_CURVE ( 'NONE', #3879, #1683, #94, .T. ) ;
#1087=CONICAL_SURFACE ( 'NONE', #1815, 0.3543307086614173596, 1.047197551196596521 ) ;
#1088=LINE ( 'NONE', #5499, #1099 ) ;
#1092=CARTESIAN_POINT ( 'NONE',  ( 3.414809992080329023E-17, 0.4091458600556405201, -0.03164754241312491001 ) ) ;
#1095=ORIENTED_EDGE ( 'NONE', *, *, #6551, .T. ) ;
#1099=VECTOR ( 'NONE', #5457, 39.37007874015748143 ) ;
#1101=DIRECTION ( 'NONE',  ( -1.000000000000000000, 0.000000000000000000, 0.000000000000000000 ) ) ;
#1108=VERTEX_POINT ( 'NONE', #3632 ) ;
#1109=CARTESIAN_POINT ( 'NONE',  ( 0.3543307086614173040, 0.2045729300278199825, -0.4082677165354330340 ) ) ;
#1113=CONICAL_SURFACE ( 'NONE', #3691, 0.3543307086614173596, 1.047197551196596521 ) ;
#1118=CARTESIAN_POINT ( 'NONE',  ( -0.3543307086614173040, 0.2045729300278199547, -0.03164754241312472960 ) ) ;
#1137=CARTESIAN_POINT ( 'NONE',  ( -0.2371803407075529779, -0.2722097265016479306, -0.4046248963849241043 ) ) ;
#1144=CARTESIAN_POINT ( 'NONE',  ( 3.414809992080329023E-17, 0.4091458600556405201, -0.3766201741223081378 ) ) ;
#1149=ADVANCED_FACE ( 'NONE', ( #596 ), #6529, .T. ) ;
#1152=DIRECTION ( 'NONE',  ( 0.000000000000000000, 0.000000000000000000, -1.000000000000000000 ) ) ;
#1159=CARTESIAN_POINT ( 'NONE',  ( 0.000000000000000000, 0.000000000000000000, -0.4082677165354330340 ) ) ;
#1166=DIRECTION ( 'NONE',  ( -1.000000000000000000, 0.000000000000000000, 0.000000000000000000 ) ) ;
#1173=B_SPLINE_CURVE_WITH_KNOTS ( 'NONE', 3,
 ( #235, #3207, #6691, #5477, #2555, #1434 ),
 .UNSPECIFIED., .F., .F.,
 ( 4, 2, 4 ),
 ( 2.380730968201871590E-07, 0.002629065763328350055, 0.005257893453559879353 ),
 .UNSPECIFIED. ) ;
#1188=B_SPLINE_CURVE_WITH_KNOTS ( 'NONE', 3,
 ( #4271, #6609, #1358, #5082, #5120, #3854 ),
 .UNSPECIFIED., .F., .F.,
 ( 4, 2, 4 ),
 ( 2.380730968228139670E-07, 0.002629065763328361331, 0.005257893453559899302 ),
 .UNSPECIFIED. ) ;
#1199=EDGE_CURVE ( 'NONE', #5611, #1, #5894, .T. ) ;
#1202=DIRECTION ( 'NONE',  ( 0.000000000000000000, -0.000000000000000000, 1.000000000000000000 ) ) ;
#1215=ORIENTED_EDGE ( 'NONE', *, *, #2294, .T. ) ;
#1236=CARTESIAN_POINT ( 'NONE',  ( 0.3543307086614172485, 0.000000000000000000, 7.886165872636028972E-17 ) ) ;
#1242=ORIENTED_EDGE ( 'NONE', *, *, #946, .F. ) ;
#1249=ORIENTED_EDGE ( 'NONE', *, *, #2569, .T. ) ;
#1250=CARTESIAN_POINT ( 'NONE',  ( 0.1621299108466741079, -0.3155401123846236500, -3.166369226054953705E-17 ) ) ;
#1253=EDGE_LOOP ( 'NONE', ( #516, #1922 ) ) ;
#1256=FACE_OUTER_BOUND ( 'NONE', #7123, .T. ) ;
#1262=CARTESIAN_POINT ( 'NONE',  ( 0.000000000000000000, 0.000000000000000000, 0.3732633159281743551 ) ) ;
#1268=ORIENTED_EDGE ( 'NONE', *, *, #5904, .T. ) ;
#1270=CYLINDRICAL_SURFACE ( 'NONE', #6715, 0.2699662542182227343 ) ;
#1278=DIRECTION ( 'NONE',  ( 1.000000000000000000, 0.000000000000000000, 0.000000000000000000 ) ) ;
#1282=EDGE_LOOP ( 'NONE', ( #4826, #6098, #395 ) ) ;
#1284=DIRECTION ( 'NONE',  ( 0.000000000000000000, 0.000000000000000000, -1.000000000000000000 ) ) ;
#1294=CARTESIAN_POINT ( 'NONE',  ( -0.3543307086614173040, -0.1372236123666514540, -0.01398679180475823590 ) ) ;
#1296=VERTEX_POINT ( 'NONE', #5627 ) ;
#1303=CARTESIAN_POINT ( 'NONE',  ( 0.3543307086614173596, 0.000000000000000000, -0.4082677165354330340 ) ) ;
#1322=CARTESIAN_POINT ( 'NONE',  ( -0.1922007978147441398, -0.2981786776988375465, -2.347681869555223892E-17 ) ) ;
#1342=LENGTH_MEASURE_WITH_UNIT ( LENGTH_MEASURE( 0.02539999999999999897 ), #7503 );
#1346=AXIS2_PLACEMENT_3D ( 'NONE', #1462, #7321, #4349 ) ;
#1347=LENGTH_MEASURE_WITH_UNIT ( LENGTH_MEASURE( 0.02539999999999999897 ), #4227 );
#1350=CARTESIAN_POINT ( 'NONE',  ( 0.3543307086614173040, 0.1714946277491099791, -0.02209865905065017816 ) ) ;
#1358=CARTESIAN_POINT ( 'NONE',  ( 0.05817553349160910214, 0.3755582001340100340, -0.01402797064541879898 ) ) ;
#1365=ORIENTED_EDGE ( 'NONE', *, *, #7283, .T. ) ;
#1369=EDGE_LOOP ( 'NONE', ( #1958, #2983, #132, #1571, #1534, #6317 ) ) ;
#1377=B_SPLINE_CURVE_WITH_KNOTS ( 'NONE', 3,
 ( #5855, #4562, #2866, #5719, #2831, #2295 ),
 .UNSPECIFIED., .F., .F.,
 ( 4, 2, 4 ),
 ( 2.380730968220726014E-07, 0.002629065763328353091, 0.005257893453559884557 ),
 .UNSPECIFIED. ) ;
#1378=VERTEX_POINT ( 'NONE', #4645 ) ;
#1398=CARTESIAN_POINT ( 'NONE',  ( -0.2520187439128739881, -0.2636427704167116359, -0.005786797686151756714 ) ) ;
#1416=CARTESIAN_POINT ( 'NONE',  ( -0.3543307086614173040, -0.1372236123666514263, -0.3942809247306748865 ) ) ;
#1418=( NAMED_UNIT ( * ) PLANE_ANGLE_UNIT ( ) SI_UNIT ( $, .RADIAN. ) );
#1419=VERTEX_POINT ( 'NONE', #6944 ) ;
#1420=( CONVERSION_BASED_UNIT ( 'INCH', #1347 ) LENGTH_UNIT ( ) NAMED_UNIT ( #5712 ) );
#1422=FACE_OUTER_BOUND ( 'NONE', #6071, .T. ) ;
#1423=FACE_OUTER_BOUND ( 'NONE', #4511, .T. ) ;
#1432=ORIENTED_EDGE ( 'NONE', *, *, #2059, .T. ) ;
#1434=CARTESIAN_POINT ( 'NONE',  ( 0.1771653543307089296, -0.3068593950417301541, -0.4082677165354330340 ) ) ;
#1438=EDGE_CURVE ( 'NONE', #1762, #2951, #3304, .T. ) ;
#1456=ORIENTED_EDGE ( 'NONE', *, *, #2885, .T. ) ;
#1462=CARTESIAN_POINT ( 'NONE',  ( 0.000000000000000000, 0.2699662542182227343, 0.1783464566929134354 ) ) ;
#1474=CARTESIAN_POINT ( 'NONE',  ( -0.1470270249832137943, 0.3242597676034320586, -0.0007480297793123595346 ) ) ;
#1476=CIRCLE ( 'NONE', #5168, 0.05944881889763781874 ) ;
#1488=DIRECTION ( 'NONE',  ( 0.000000000000000000, -1.000000000000000000, 0.000000000000000000 ) ) ;
#1512=CARTESIAN_POINT ( 'NONE',  ( 0.000000000000000000, 0.000000000000000000, -0.4082677165354330340 ) ) ;
#1522=EDGE_LOOP ( 'NONE', ( #7339, #2572, #3193, #6564, #6097, #5636 ) ) ;
#1526=DIRECTION ( 'NONE',  ( 1.000000000000000000, 0.000000000000000000, 0.000000000000000000 ) ) ;
#1534=ORIENTED_EDGE ( 'NONE', *, *, #4718, .T. ) ;
#1542=EDGE_CURVE ( 'NONE', #662, #1296, #1625, .T. ) ;
#1543=CARTESIAN_POINT ( 'NONE',  ( -0.3543307086614173040, 0.2045729300278205931, -0.3766201741223081378 ) ) ;
#1550=CIRCLE ( 'NONE', #2536, 0.2362204724409449619 ) ;
#1555=DIRECTION ( 'NONE',  ( 0.000000000000000000, 0.000000000000000000, -1.000000000000000000 ) ) ;
#1562=DIRECTION ( 'NONE',  ( -0.000000000000000000, -0.000000000000000000, 1.000000000000000000 ) ) ;
#1563=VECTOR ( 'NONE', #1988, 39.37007874015748143 ) ;
#1564=B_SPLINE_CURVE_WITH_KNOTS ( 'NONE', 3,
 ( #2083, #3222, #2608, #7306, #5495, #290 ),
 .UNSPECIFIED., .F., .F.,
 ( 4, 2, 4 ),
 ( 2.380730968505120768E-07, 0.002629065763328379546, 0.005257893453559907976 ),
 .UNSPECIFIED. ) ;
#1571=ORIENTED_EDGE ( 'NONE', *, *, #1681, .T. ) ;
#1576=EDGE_CURVE ( 'NONE', #4172, #2074, #2775, .T. ) ;
#1596=EDGE_CURVE ( 'NONE', #1, #3631, #4215, .T. ) ;
#1612=AXIS2_PLACEMENT_3D ( 'NONE', #5740, #6304, #5167 ) ;
#1625=CIRCLE ( 'NONE', #907, 0.3543307086614173596 ) ;
#1628=CARTESIAN_POINT ( 'NONE',  ( -0.2362204724409449619, 0.000000000000000000, -0.4072677165354330331 ) ) ;
#1636=ADVANCED_FACE ( 'NONE', ( #5328 ), #1891, .F. ) ;
#1643=DIMENSIONAL_EXPONENTS ( 1.000000000000000000, 0.000000000000000000, 0.000000000000000000, 0.000000000000000000, 0.000000000000000000, 0.000000000000000000, 0.000000000000000000 ) ;
#1645=CYLINDRICAL_SURFACE ( 'NONE', #4436, 0.2362204724409449619 ) ;
#1662=CARTESIAN_POINT ( 'NONE',  ( 0.1469816153540864645, 0.3242859848650325727, -0.4082677165354333115 ) ) ;
#1673=DIRECTION ( 'NONE',  ( -1.000000000000000000, 0.000000000000000000, -0.000000000000000000 ) ) ;
#1675=FACE_OUTER_BOUND ( 'NONE', #1522, .T. ) ;
#1681=EDGE_CURVE ( 'NONE', #3999, #929, #2570, .T. ) ;
#1683=VERTEX_POINT ( 'NONE', #1798 ) ;
#1694=CIRCLE ( 'NONE', #2191, 0.2699662542182227343 ) ;
#1700=CARTESIAN_POINT ( 'NONE',  ( -0.3543307086614173040, 0.000000000000000000, 7.886165872636028972E-17 ) ) ;
#1710=ORIENTED_EDGE ( 'NONE', *, *, #3316, .T. ) ;
#1725=CONICAL_SURFACE ( 'NONE', #3322, 0.3543307086614173596, 1.047197551196596521 ) ;
#1731=EDGE_CURVE ( 'NONE', #1683, #2077, #1564, .T. ) ;
#1754=EDGE_CURVE ( 'NONE', #5614, #5707, #4950, .T. ) ;
#1758=CARTESIAN_POINT ( 'NONE',  ( 0.3543307086614173040, 0.1714946277491099791, -0.3861690574847828072 ) ) ;
#1762=VERTEX_POINT ( 'NONE', #3799 ) ;
#1784=CARTESIAN_POINT ( 'NONE',  ( -0.2066929133858267931, 2.531258147843938473E-17, -0.3865922971001068409 ) ) ;
#1786=DIRECTION ( 'NONE',  ( -0.000000000000000000, -0.000000000000000000, 1.000000000000000000 ) ) ;
#1798=CARTESIAN_POINT ( 'NONE',  ( -9.561467977824920278E-16, -0.4091458600556405756, -0.03164754241312491001 ) ) ;
#1808=CONICAL_SURFACE ( 'NONE', #7436, 0.3543307086614173596, 1.047197551196596521 ) ;
#1810=CARTESIAN_POINT ( 'NONE',  ( 0.3543307086614173596, -0.2045729300278204543, -0.3766201741223081378 ) ) ;
#1815=AXIS2_PLACEMENT_3D ( 'NONE', #5943, #4864, #2076 ) ;
#1826=ORIENTED_EDGE ( 'NONE', *, *, #3982, .T. ) ;
#1827=CIRCLE ( 'NONE', #6347, 0.05944881889763779792 ) ;
#1830=ORIENTED_EDGE ( 'NONE', *, *, #2207, .T. ) ;
#1849=UNCERTAINTY_MEASURE_WITH_UNIT (LENGTH_MEASURE( 1.000000000000000082E-05 ), #3109, 'distance_accuracy_value', 'NONE');
#1856=FACE_OUTER_BOUND ( 'NONE', #5913, .T. ) ;
#1868=DIRECTION ( 'NONE',  ( -1.000000000000000000, 0.000000000000000000, 0.000000000000000000 ) ) ;
#1872=CONICAL_SURFACE ( 'NONE', #6269, 0.2362204724409449619, 0.9599310885968795892 ) ;
#1875=ORIENTED_EDGE ( 'NONE', *, *, #3882, .F. ) ;
#1889=CARTESIAN_POINT ( 'NONE',  ( 0.000000000000000000, 0.000000000000000000, -0.4082677165354330340 ) ) ;
#1891=CYLINDRICAL_SURFACE ( 'NONE', #2298, 0.2066929133858267931 ) ;
#1898=CARTESIAN_POINT ( 'NONE',  ( 0.000000000000000000, 0.000000000000000000, 0.000000000000000000 ) ) ;
#1906=DIRECTION ( 'NONE',  ( 0.000000000000000000, -0.000000000000000000, 1.000000000000000000 ) ) ;
#1907=CARTESIAN_POINT ( 'NONE',  ( 0.3543307086614173596, -0.2045729300278204543, -0.03164754241312491001 ) ) ;
#1922=ORIENTED_EDGE ( 'NONE', *, *, #5334, .T. ) ;
#1930=CIRCLE ( 'NONE', #5474, 0.3543307086614173596 ) ;
#1933=ORIENTED_EDGE ( 'NONE', *, *, #3316, .F. ) ;
#1958=ORIENTED_EDGE ( 'NONE', *, *, #2885, .F. ) ;
#1963=CARTESIAN_POINT ( 'NONE',  ( 0.3253487914207032761, -0.2213056477483782425, -0.02198690333287102797 ) ) ;
#1964=ORIENTED_EDGE ( 'NONE', *, *, #5478, .T. ) ;
#1968=CARTESIAN_POINT ( 'NONE',  ( -0.3543307086614173040, 0.000000000000000000, -0.4082677165354330340 ) ) ;
#1985=FACE_OUTER_BOUND ( 'NONE', #4298, .T. ) ;
#1988=DIRECTION ( 'NONE',  ( 0.000000000000000000, 0.000000000000000000, 1.000000000000000000 ) ) ;
#1992=AXIS2_PLACEMENT_3D ( 'NONE', #5022, #2075, #7226 ) ;
#2001=ORIENTED_EDGE ( 'NONE', *, *, #1754, .F. ) ;
#2031=DIRECTION ( 'NONE',  ( -1.000000000000000000, 0.000000000000000000, 0.000000000000000000 ) ) ;
#2052=CARTESIAN_POINT ( 'NONE',  ( 0.2066929133858267931, 0.000000000000000000, -0.3865922971001068409 ) ) ;
#2053=ADVANCED_FACE ( 'NONE', ( #2515 ), #6083, .T. ) ;
#2059=EDGE_CURVE ( 'NONE', #6553, #2951, #6008, .T. ) ;
#2067=EDGE_LOOP ( 'NONE', ( #3836, #2637, #1875, #2411 ) ) ;
#2068=VECTOR ( 'NONE', #5990, 39.37007874015748143 ) ;
#2069=CARTESIAN_POINT ( 'NONE',  ( -0.1621299108466738859, 0.3155401123846230949, 2.446057743350508180E-16 ) ) ;
#2074=VERTEX_POINT ( 'NONE', #3167 ) ;
#2075=DIRECTION ( 'NONE',  ( -0.000000000000000000, -0.000000000000000000, 1.000000000000000000 ) ) ;
#2076=DIRECTION ( 'NONE',  ( 1.000000000000000000, 0.000000000000000000, 0.000000000000000000 ) ) ;
#2077=VERTEX_POINT ( 'NONE', #5512 ) ;
#2083=CARTESIAN_POINT ( 'NONE',  ( -9.561467977824920278E-16, -0.4091458600556405756, -0.03164754241312491001 ) ) ;
#2084=ORIENTED_EDGE ( 'NONE', *, *, #6446, .F. ) ;
#2087=AXIS2_PLACEMENT_3D ( 'NONE', #4032, #6367, #5798 ) ;
#2105=AXIS2_PLACEMENT_3D ( 'NONE', #5800, #5257, #5869 ) ;
#2115=CIRCLE ( 'NONE', #5170, 0.2362204724409449619 ) ;
#2122=EDGE_LOOP ( 'NONE', ( #2794, #5563, #5711 ) ) ;
#2126=EDGE_LOOP ( 'NONE', ( #860, #5073, #328 ) ) ;
#2134=DIRECTION ( 'NONE',  ( 0.000000000000000000, 0.000000000000000000, 1.000000000000000000 ) ) ;
#2136=PLANE ( 'NONE',  #4877 ) ;
#2138=CARTESIAN_POINT ( 'NONE',  ( -1.126887297386508504E-15, -0.4091458600556405756, -0.3766201741223081378 ) ) ;
#2152=ADVANCED_FACE ( 'NONE', ( #3120 ), #5119, .T. ) ;
#2188=ORIENTED_EDGE ( 'NONE', *, *, #7005, .F. ) ;
#2189=CARTESIAN_POINT ( 'NONE',  ( 0.2948818897637794367, 0.000000000000000000, 0.1188976377952756375 ) ) ;
#2191=AXIS2_PLACEMENT_3D ( 'NONE', #5007, #4392, #2628 ) ;
#2207=EDGE_CURVE ( 'NONE', #3331, #4739, #2992, .T. ) ;
#2238=CIRCLE ( 'NONE', #1992, 0.2699662542182227343 ) ;
#2261=DIRECTION ( 'NONE',  ( 1.000000000000000000, 0.000000000000000000, 0.000000000000000000 ) ) ;
#2266=VERTEX_POINT ( 'NONE', #7372 ) ;
#2272=CARTESIAN_POINT ( 'NONE',  ( -0.05806029764938282212, 0.3756247315785394836, -0.3942118233966397933 ) ) ;
#2284=VECTOR ( 'NONE', #3018, 39.37007874015748143 ) ;
#2288=ORIENTED_EDGE ( 'NONE', *, *, #2769, .T. ) ;
#2291=VECTOR ( 'NONE', #5435, 39.37007874015748143 ) ;
#2294=EDGE_CURVE ( 'NONE', #5092, #7286, #3382, .T. ) ;
#2295=CARTESIAN_POINT ( 'NONE',  ( -0.1771653543307089573, 0.3068593950417301541, 0.000000000000000000 ) ) ;
#2296=DIRECTION ( 'NONE',  ( -0.000000000000000000, -0.000000000000000000, 1.000000000000000000 ) ) ;
#2298=AXIS2_PLACEMENT_3D ( 'NONE', #88, #7007, #4797 ) ;
#2299=FACE_OUTER_BOUND ( 'NONE', #3723, .T. ) ;
#2300=DIRECTION ( 'NONE',  ( 0.5000000000000006661, -0.8660254037844382635, 0.000000000000000000 ) ) ;
#2302=EDGE_LOOP ( 'NONE', ( #182, #3445 ) ) ;
#2312=FACE_OUTER_BOUND ( 'NONE', #3182, .T. ) ;
#2320=EDGE_CURVE ( 'NONE', #6033, #4139, #5641, .T. ) ;
#2325=FACE_OUTER_BOUND ( 'NONE', #1282, .T. ) ;
#2338=FACE_OUTER_BOUND ( 'NONE', #1369, .T. ) ;
#2342=ORIENTED_EDGE ( 'NONE', *, *, #4867, .T. ) ;
#2349=CARTESIAN_POINT ( 'NONE',  ( -0.3543307086614173596, 0.03458999977076007704, 3.331440607508054140E-17 ) ) ;
#2364=EDGE_CURVE ( 'NONE', #1068, #5707, #6877, .T. ) ;
#2374=ADVANCED_FACE ( 'NONE', ( #6760, #343 ), #2136, .T. ) ;
#2393=DIRECTION ( 'NONE',  ( 1.000000000000000000, 0.000000000000000000, 0.000000000000000000 ) ) ;
#2400=DIRECTION ( 'NONE',  ( 1.000000000000000000, 0.000000000000000000, 0.000000000000000000 ) ) ;
#2406=VERTEX_POINT ( 'NONE', #2514 ) ;
#2410=ORIENTED_EDGE ( 'NONE', *, *, #3982, .F. ) ;
#2411=ORIENTED_EDGE ( 'NONE', *, *, #851, .F. ) ;
#2417=CARTESIAN_POINT ( 'NONE',  ( 0.3543307086614173596, 0.03458999977076007010, -0.4082677165354332005 ) ) ;
#2421=EDGE_LOOP ( 'NONE', ( #4123, #6145, #6786 ) ) ;
#2423=EDGE_CURVE ( 'NONE', #4931, #3999, #2678, .T. ) ;
#2428=CARTESIAN_POINT ( 'NONE',  ( 0.000000000000000000, 0.000000000000000000, -0.4072677165354330331 ) ) ;
#2440=CARTESIAN_POINT ( 'NONE',  ( 0.000000000000000000, 0.000000000000000000, -0.4082677165354330340 ) ) ;
#2450=TOROIDAL_SURFACE ( 'NONE', #5871, 0.2948818897637794367, 0.05944881889763781874 ) ;
#2454=CARTESIAN_POINT ( 'NONE',  ( -0.1771653543307089573, 0.3068593950417301541, -0.4082677165354330340 ) ) ;
#2464=ORIENTED_EDGE ( 'NONE', *, *, #340, .T. ) ;
#2468=CARTESIAN_POINT ( 'NONE',  ( 0.3543307086614173040, 0.1379824317933223410, -0.01414634932344265711 ) ) ;
#2474=APPLICATION_CONTEXT ( 'automotive_design' ) ;
#2479=EDGE_CURVE ( 'NONE', #5128, #4225, #4512, .T. ) ;
#2497=ORIENTED_EDGE ( 'NONE', *, *, #6551, .F. ) ;
#2514=CARTESIAN_POINT ( 'NONE',  ( -0.2948818897637794922, 3.975280653137765506E-17, 0.1783464566929134354 ) ) ;
#2515=FACE_OUTER_BOUND ( 'NONE', #7214, .T. ) ;
#2523=ORIENTED_EDGE ( 'NONE', *, *, #946, .T. ) ;
#2535=DIRECTION ( 'NONE',  ( -0.000000000000000000, -0.000000000000000000, 1.000000000000000000 ) ) ;
#2536=AXIS2_PLACEMENT_3D ( 'NONE', #657, #618, #5357 ) ;
#2549=DIRECTION ( 'NONE',  ( -1.000000000000000000, 0.000000000000000000, 0.000000000000000000 ) ) ;
#2555=CARTESIAN_POINT ( 'NONE',  ( 0.2073490933073313947, -0.2894328052184282352, -0.4082677165354329785 ) ) ;
#2566=ORIENTED_EDGE ( 'NONE', *, *, #1542, .F. ) ;
#2569=EDGE_CURVE ( 'NONE', #3513, #6033, #1694, .T. ) ;
#2570=B_SPLINE_CURVE_WITH_KNOTS ( 'NONE', 3,
 ( #1303, #2417, #5292, #2948, #1758, #131 ),
 .UNSPECIFIED., .F., .F.,
 ( 4, 2, 4 ),
 ( 0.01452727543195640389, 0.01715716534226973539, 0.01978705525258306688 ),
 .UNSPECIFIED. ) ;
#2572=ORIENTED_EDGE ( 'NONE', *, *, #1731, .T. ) ;
#2573=CIRCLE ( 'NONE', #4411, 0.3543307086614173596 ) ;
#2574=CARTESIAN_POINT ( 'NONE',  ( -0.3543307086614173040, -0.2045729300278205931, -0.3766201741223081378 ) ) ;
#2601=ORIENTED_EDGE ( 'NONE', *, *, #4154, .T. ) ;
#2608=CARTESIAN_POINT ( 'NONE',  ( -0.05817553349160980991, -0.3755582001340100895, -0.01402797064541895684 ) ) ;
#2611=DIRECTION ( 'NONE',  ( 1.000000000000000000, 0.000000000000000000, 0.000000000000000000 ) ) ;
#2618=( NAMED_UNIT ( * ) PLANE_ANGLE_UNIT ( ) SI_UNIT ( $, .RADIAN. ) );
#2622=DIRECTION ( 'NONE',  ( -1.000000000000000000, 0.000000000000000000, 0.000000000000000000 ) ) ;
#2628=DIRECTION ( 'NONE',  ( 1.000000000000000000, 0.000000000000000000, 0.000000000000000000 ) ) ;
#2629=ORIENTED_EDGE ( 'NONE', *, *, #6273, .T. ) ;
#2633=B_SPLINE_CURVE_WITH_KNOTS ( 'NONE', 3,
 ( #892, #1963, #3221, #7345, #3763, #7233 ),
 .UNSPECIFIED., .F., .F.,
 ( 4, 2, 4 ),
 ( 2.380730968201100790E-07, 0.002629065763328349622, 0.005257893453559878486 ),
 .UNSPECIFIED. ) ;
#2635=CARTESIAN_POINT ( 'NONE',  ( 0.000000000000000000, 0.000000000000000000, 0.3732633159281743551 ) ) ;
#2637=ORIENTED_EDGE ( 'NONE', *, *, #3416, .T. ) ;
#2641=PRODUCT_DEFINITION_SHAPE ( 'NONE', 'NONE',  #558 ) ;
#2649=ORIENTED_EDGE ( 'NONE', *, *, #3070, .F. ) ;
#2653=CARTESIAN_POINT ( 'NONE',  ( 0.2362204724409449619, 2.892866454678788147E-17, -0.4072677165354330331 ) ) ;
#2656=CARTESIAN_POINT ( 'NONE',  ( 0.1771653543307089296, 0.3068593950417301541, -0.4082677165354330340 ) ) ;
#2678=B_SPLINE_CURVE_WITH_KNOTS ( 'NONE', 3,
 ( #3669, #4275, #724, #5930, #3090, #5393 ),
 .UNSPECIFIED., .F., .F.,
 ( 4, 2, 4 ),
 ( 0.009270618776430220032, 0.01189894710419331196, 0.01452727543195640389 ),
 .UNSPECIFIED. ) ;
#2694=AXIS2_PLACEMENT_3D ( 'NONE', #784, #5373, #3610 ) ;
#2695=FACE_OUTER_BOUND ( 'NONE', #2760, .T. ) ;
#2698=CARTESIAN_POINT ( 'NONE',  ( -0.3543307086614173040, 0.1714946277491101179, -0.3861690574847828072 ) ) ;
#2706=AXIS2_PLACEMENT_3D ( 'NONE', #7201, #4996, #4420 ) ;
#2713=CARTESIAN_POINT ( 'NONE',  ( 0.1922007978147437512, 0.2981786776988370469, -0.4082677165354333670 ) ) ;
#2731=CARTESIAN_POINT ( 'NONE',  ( -0.3254211578371892788, -0.2212638669783397183, -0.3862566910637255102 ) ) ;
#2741=DIRECTION ( 'NONE',  ( 1.000000000000000000, 0.000000000000000000, 0.000000000000000000 ) ) ;
#2749=DIRECTION ( 'NONE',  ( -0.5000000000000006661, -0.8660254037844383745, 0.000000000000000000 ) ) ;
#2756=ORIENTED_EDGE ( 'NONE', *, *, #2294, .F. ) ;
#2758=DIRECTION ( 'NONE',  ( 0.000000000000000000, 0.000000000000000000, -1.000000000000000000 ) ) ;
#2759=CARTESIAN_POINT ( 'NONE',  ( -0.2699662542182227343, 3.306133091061471023E-17, 0.1783464566929134354 ) ) ;
#2760=EDGE_LOOP ( 'NONE', ( #554, #2464, #7485 ) ) ;
#2763=DIRECTION ( 'NONE',  ( -0.000000000000000000, -0.000000000000000000, 1.000000000000000000 ) ) ;
#2769=EDGE_CURVE ( 'NONE', #4410, #1296, #1188, .T. ) ;
#2775=LINE ( 'NONE', #5157, #4012 ) ;
#2776=CARTESIAN_POINT ( 'NONE',  ( -0.3543307086614173596, 0.03458999977076020194, -0.4082677165354332005 ) ) ;
#2781=CARTESIAN_POINT ( 'NONE',  ( 0.000000000000000000, 0.000000000000000000, -0.4082677165354330340 ) ) ;
#2794=ORIENTED_EDGE ( 'NONE', *, *, #5242, .T. ) ;
#2795=CARTESIAN_POINT ( 'NONE',  ( 0.3543307086614173040, 0.2045729300278205931, -0.03164754241312491001 ) ) ;
#2797=ADVANCED_FACE ( 'NONE', ( #1256 ), #1087, .T. ) ;
#2799=EDGE_LOOP ( 'NONE', ( #1249, #2342 ) ) ;
#2802=DIRECTION ( 'NONE',  ( -0.000000000000000000, -0.000000000000000000, 1.000000000000000000 ) ) ;
#2803=EDGE_LOOP ( 'NONE', ( #3242, #1215, #6993, #4120 ) ) ;
#2810=CONICAL_SURFACE ( 'NONE', #7441, 0.3543307086614173596, 1.047197551196596521 ) ;
#2811=ADVANCED_FACE ( 'NONE', ( #967 ), #6949, .T. ) ;
#2816=DIRECTION ( 'NONE',  ( 0.000000000000000000, 0.000000000000000000, 1.000000000000000000 ) ) ;
#2825=AXIS2_PLACEMENT_3D ( 'NONE', #62, #1152, #3581 ) ;
#2831=CARTESIAN_POINT ( 'NONE',  ( -0.2073490933073312559, 0.2894328052184277356, 2.399704365528325123E-16 ) ) ;
#2843=B_SPLINE_CURVE_WITH_KNOTS ( 'NONE', 3,
 ( #500, #2776, #3386, #4467, #2698, #1543 ),
 .UNSPECIFIED., .F., .F.,
 ( 4, 2, 4 ),
 ( 0.01452727543195640389, 0.01715716534226973539, 0.01978705525258306688 ),
 .UNSPECIFIED. ) ;
#2844=DIRECTION ( 'NONE',  ( -0.000000000000000000, -0.000000000000000000, 1.000000000000000000 ) ) ;
#2866=CARTESIAN_POINT ( 'NONE',  ( -0.2961551751698085488, 0.2381605899494505241, -0.01402797064541873306 ) ) ;
#2868=ORIENTED_EDGE ( 'NONE', *, *, #3542, .T. ) ;
#2875=CARTESIAN_POINT ( 'NONE',  ( -0.1621299108466738859, 0.3155401123846230949, -0.4082677165354333115 ) ) ;
#2885=EDGE_CURVE ( 'NONE', #4654, #662, #6694, .T. ) ;
#2895=CIRCLE ( 'NONE', #6440, 0.3543307086614173596 ) ;
#2898=CARTESIAN_POINT ( 'NONE',  ( 0.000000000000000000, 0.000000000000000000, 0.1188976377952756375 ) ) ;
#2905=CARTESIAN_POINT ( 'NONE',  ( 0.2699662542182227343, 0.000000000000000000, 0.3732633159281743551 ) ) ;
#2911=CARTESIAN_POINT ( 'NONE',  ( 0.000000000000000000, 0.000000000000000000, -0.4072677165354330331 ) ) ;
#2920=CARTESIAN_POINT ( 'NONE',  ( -0.1171731013849884873, -0.3414959384292345357, -0.4052515342986934832 ) ) ;
#2942=ORIENTED_EDGE ( 'NONE', *, *, #3882, .T. ) ;
#2948=CARTESIAN_POINT ( 'NONE',  ( 0.3543307086614173040, 0.1379824317933222577, -0.3941213672119904809 ) ) ;
#2949=CARTESIAN_POINT ( 'NONE',  ( 0.2066929133858267931, 0.000000000000000000, -0.4082677165354330340 ) ) ;
#2951=VERTEX_POINT ( 'NONE', #1118 ) ;
#2961=PRODUCT_DEFINITION_CONTEXT ( 'detailed design', #4972, 'design' ) ;
#2983=ORIENTED_EDGE ( 'NONE', *, *, #4154, .F. ) ;
#2984=CYLINDRICAL_SURFACE ( 'NONE', #5538, 0.2699662542182227343 ) ;
#2992=LINE ( 'NONE', #2949, #2068 ) ;
#3003=FACE_OUTER_BOUND ( 'NONE', #4049, .T. ) ;
#3017=AXIS2_PLACEMENT_3D ( 'NONE', #6911, #2296, #1526 ) ;
#3018=DIRECTION ( 'NONE',  ( 0.000000000000000000, 0.000000000000000000, 1.000000000000000000 ) ) ;
#3025=DIRECTION ( 'NONE',  ( 0.000000000000000000, -0.000000000000000000, 1.000000000000000000 ) ) ;
#3035=ADVANCED_FACE ( 'NONE', ( #1985 ), #1808, .T. ) ;
#3047=DIRECTION ( 'NONE',  ( -1.000000000000000000, 0.000000000000000000, 0.000000000000000000 ) ) ;
#3067=ORIENTED_EDGE ( 'NONE', *, *, #1542, .T. ) ;
#3070=EDGE_CURVE ( 'NONE', #2266, #3999, #7069, .T. ) ;
#3080=CARTESIAN_POINT ( 'NONE',  ( 3.414809992080329023E-17, 0.4091458600556405201, -0.3766201741223081378 ) ) ;
#3090=CARTESIAN_POINT ( 'NONE',  ( 0.3543307086614173040, -0.03456946083495027883, -0.4082677165354330895 ) ) ;
#3095=LINE ( 'NONE', #5441, #522 ) ;
#3109=( CONVERSION_BASED_UNIT ( 'INCH', #1342 ) LENGTH_UNIT ( ) NAMED_UNIT ( #1643 ) );
#3120=FACE_OUTER_BOUND ( 'NONE', #2122, .T. ) ;
#3127=CARTESIAN_POINT ( 'NONE',  ( 0.1621299108466740524, -0.3155401123846237055, -0.4082677165354329785 ) ) ;
#3128=CARTESIAN_POINT ( 'NONE',  ( 0.000000000000000000, 0.000000000000000000, -0.3865922971001068409 ) ) ;
#3130=ORIENTED_EDGE ( 'NONE', *, *, #4155, .T. ) ;
#3147=CARTESIAN_POINT ( 'NONE',  ( -0.2362204724409449619, 2.892866454678788147E-17, -0.9857285720115422922 ) ) ;
#3149=CIRCLE ( 'NONE', #4118, 0.3543307086614173596 ) ;
#3165=CARTESIAN_POINT ( 'NONE',  ( -0.2371803407075528947, -0.2722097265016478751, -0.003642820150508878103 ) ) ;
#3167=CARTESIAN_POINT ( 'NONE',  ( -0.3543307086614173040, -0.2045729300278205931, -0.03164754241312491001 ) ) ;
#3181=ADVANCED_FACE ( 'NONE', ( #4062 ), #6393, .T. ) ;
#3182=EDGE_LOOP ( 'NONE', ( #5362, #1070, #475, #2084 ) ) ;
#3190=ORIENTED_EDGE ( 'NONE', *, *, #701, .F. ) ;
#3193=ORIENTED_EDGE ( 'NONE', *, *, #4676, .T. ) ;
#3202=TOROIDAL_SURFACE ( 'NONE', #6023, 0.2948818897637794367, 0.05944881889763781874 ) ;
#3206=CARTESIAN_POINT ( 'NONE',  ( -0.3543307086614173040, 0.2045729300278199547, -0.4082677165354330340 ) ) ;
#3207=CARTESIAN_POINT ( 'NONE',  ( 0.3253487914207032761, -0.2213056477483782147, -0.3862808132025620234 ) ) ;
#3213=EDGE_LOOP ( 'NONE', ( #2601, #1826, #3612, #6502, #406, #6241 ) ) ;
#3221=CARTESIAN_POINT ( 'NONE',  ( 0.2961551751698085488, -0.2381605899494510792, -0.01402797064541896205 ) ) ;
#3222=CARTESIAN_POINT ( 'NONE',  ( -0.02898191724071497513, -0.3924131423350826764, -0.02198690333287099327 ) ) ;
#3225=DIRECTION ( 'NONE',  ( -0.000000000000000000, -0.000000000000000000, 1.000000000000000000 ) ) ;
#3242=ORIENTED_EDGE ( 'NONE', *, *, #3416, .F. ) ;
#3257=ORIENTED_EDGE ( 'NONE', *, *, #7283, .F. ) ;
#3263=EDGE_LOOP ( 'NONE', ( #37, #4627 ) ) ;
#3279=CARTESIAN_POINT ( 'NONE',  ( 0.1470270249832138498, -0.3242597676034328358, -0.4075196867561205472 ) ) ;
#3286=CARTESIAN_POINT ( 'NONE',  ( 0.1922007978147438345, 0.2981786776988372134, 2.535346354227414414E-16 ) ) ;
#3288=DIRECTION ( 'NONE',  ( 1.000000000000000000, 0.000000000000000000, 0.000000000000000000 ) ) ;
#3291=EDGE_LOOP ( 'NONE', ( #2001, #3377, #1365, #4416 ) ) ;
#3304=B_SPLINE_CURVE_WITH_KNOTS ( 'NONE', 3,
 ( #1700, #2349, #1055, #5194, #4005, #3973 ),
 .UNSPECIFIED., .F., .F.,
 ( 4, 2, 4 ),
 ( 0.01452727543195640389, 0.01715716534226972845, 0.01978705525258304954 ),
 .UNSPECIFIED. ) ;
#3316=EDGE_CURVE ( 'NONE', #1, #5128, #4022, .T. ) ;
#3321=EDGE_CURVE ( 'NONE', #6553, #1, #4596, .T. ) ;
#3322=AXIS2_PLACEMENT_3D ( 'NONE', #3430, #672, #7088 ) ;
#3331=VERTEX_POINT ( 'NONE', #2052 ) ;
#3333=DIRECTION ( 'NONE',  ( 0.000000000000000000, 0.000000000000000000, 1.000000000000000000 ) ) ;
#3342=CARTESIAN_POINT ( 'NONE',  ( 0.000000000000000000, 0.000000000000000000, -0.9857285720115422922 ) ) ;
#3352=AXIS2_PLACEMENT_3D ( 'NONE', #4672, #7499, #5190 ) ;
#3362=VERTEX_POINT ( 'NONE', #3886 ) ;
#3364=FACE_OUTER_BOUND ( 'NONE', #2799, .T. ) ;
#3365=CARTESIAN_POINT ( 'NONE',  ( 0.2520187439128737106, 0.2636427704167112473, -0.005786797686151470485 ) ) ;
#3377=ORIENTED_EDGE ( 'NONE', *, *, #4216, .F. ) ;
#3382=CIRCLE ( 'NONE', #6220, 0.3543307086614172485 ) ;
#3386=CARTESIAN_POINT ( 'NONE',  ( -0.3543307086614173040, 0.06965032677943208683, -0.4052140698951960385 ) ) ;
#3396=CARTESIAN_POINT ( 'NONE',  ( 0.1171503679538647424, -0.3415090635818134879, -0.4046248963849241598 ) ) ;
#3407=FACE_OUTER_BOUND ( 'NONE', #6659, .T. ) ;
#3408=AXIS2_PLACEMENT_3D ( 'NONE', #2440, #1202, #3709 ) ;
#3416=EDGE_CURVE ( 'NONE', #5092, #2406, #1827, .T. ) ;
#3420=ADVANCED_FACE ( 'NONE', ( #2695 ), #2810, .T. ) ;
#3428=CARTESIAN_POINT ( 'NONE',  ( -0.1171503679538647702, 0.3415090635818126552, -0.4046248963849244373 ) ) ;
#3430=CARTESIAN_POINT ( 'NONE',  ( 0.000000000000000000, 0.000000000000000000, -0.4082677165354330340 ) ) ;
#3436=CARTESIAN_POINT ( 'NONE',  ( -0.02890955082422800443, 0.3924549231051212561, -0.02201102547170738152 ) ) ;
#3443=FACE_OUTER_BOUND ( 'NONE', #3291, .T. ) ;
#3445=ORIENTED_EDGE ( 'NONE', *, *, #562, .F. ) ;
#3446=AXIS2_PLACEMENT_3D ( 'NONE', #6960, #3516, #1101 ) ;
#3497=ORIENTED_EDGE ( 'NONE', *, *, #2207, .F. ) ;
#3499=ADVANCED_FACE ( 'NONE', ( #1856 ), #1270, .F. ) ;
#3513=VERTEX_POINT ( 'NONE', #6107 ) ;
#3516=DIRECTION ( 'NONE',  ( -0.000000000000000000, -0.000000000000000000, 1.000000000000000000 ) ) ;
#3532=DIRECTION ( 'NONE',  ( 1.000000000000000000, 0.000000000000000000, 0.000000000000000000 ) ) ;
#3541=CARTESIAN_POINT ( 'NONE',  ( -0.1469816153540869086, -0.3242859848650329058, -0.4082677165354330340 ) ) ;
#3542=EDGE_CURVE ( 'NONE', #3331, #6705, #4466, .T. ) ;
#3549=ORIENTED_EDGE ( 'NONE', *, *, #5100, .T. ) ;
#3569=ORIENTED_EDGE ( 'NONE', *, *, #6602, .T. ) ;
#3571=ORIENTED_EDGE ( 'NONE', *, *, #5109, .F. ) ;
#3573=FACE_OUTER_BOUND ( 'NONE', #7242, .T. ) ;
#3576=AXIS2_PLACEMENT_3D ( 'NONE', #1512, #3860, #6193 ) ;
#3581=DIRECTION ( 'NONE',  ( -1.000000000000000000, 0.000000000000000000, 0.000000000000000000 ) ) ;
#3589=EDGE_LOOP ( 'NONE', ( #4979, #823, #5134, #1964 ) ) ;
#3598=ORIENTED_EDGE ( 'NONE', *, *, #1576, .T. ) ;
#3599=CARTESIAN_POINT ( 'NONE',  ( -0.3543307086614173040, -0.2045729300278205931, -0.03164754241312491001 ) ) ;
#3601=ADVANCED_FACE ( 'NONE', ( #1422 ), #300, .T. ) ;
#3605=CARTESIAN_POINT ( 'NONE',  ( -0.2961551751698082713, 0.2381605899494506351, -0.3942397458900145368 ) ) ;
#3609=ORIENTED_EDGE ( 'NONE', *, *, #2479, .F. ) ;
#3610=DIRECTION ( 'NONE',  ( -1.000000000000000000, 0.000000000000000000, 0.000000000000000000 ) ) ;
#3612=ORIENTED_EDGE ( 'NONE', *, *, #1081, .T. ) ;
#3631=VERTEX_POINT ( 'NONE', #6641 ) ;
#3632=CARTESIAN_POINT ( 'NONE',  ( -0.2066929133858267931, 2.531258147843938473E-17, 0.1188976377952756375 ) ) ;
#3651=( NAMED_UNIT ( * ) SI_UNIT ( $, .STERADIAN. ) SOLID_ANGLE_UNIT ( ) );
#3655=B_SPLINE_CURVE_WITH_KNOTS ( 'NONE', 3,
 ( #3599, #6, #1294, #659, #4092, #5248 ),
 .UNSPECIFIED., .F., .F.,
 ( 4, 2, 4 ),
 ( 0.009270618776430214827, 0.01189894710419331023, 0.01452727543195640389 ),
 .UNSPECIFIED. ) ;
#3668=CARTESIAN_POINT ( 'NONE',  ( -0.2073036836782041203, -0.2894590224800286382, -0.0007480297793126502092 ) ) ;
#3669=CARTESIAN_POINT ( 'NONE',  ( 0.3543307086614173596, -0.2045729300278204543, -0.3766201741223081378 ) ) ;
#3671=ORIENTED_EDGE ( 'NONE', *, *, #1438, .F. ) ;
#3691=AXIS2_PLACEMENT_3D ( 'NONE', #4660, #6927, #1166 ) ;
#3698=CARTESIAN_POINT ( 'NONE',  ( 0.3543307086614172485, 0.000000000000000000, 7.886165872636028972E-17 ) ) ;
#3709=DIRECTION ( 'NONE',  ( -1.000000000000000000, 0.000000000000000000, 0.000000000000000000 ) ) ;
#3712=PLANE ( 'NONE',  #4800 ) ;
#3715=EDGE_LOOP ( 'NONE', ( #3598, #4973, #4909, #5750, #247, #3571 ) ) ;
#3723=EDGE_LOOP ( 'NONE', ( #6128, #3976, #3954, #3257 ) ) ;
#3728=ORIENTED_EDGE ( 'NONE', *, *, #6273, .F. ) ;
#3732=DIRECTION ( 'NONE',  ( -0.000000000000000000, -0.000000000000000000, 1.000000000000000000 ) ) ;
#3736=DIRECTION ( 'NONE',  ( -1.000000000000000000, 0.000000000000000000, 0.000000000000000000 ) ) ;
#3743=CARTESIAN_POINT ( 'NONE',  ( -0.2962704110120348289, -0.2380940585049214631, -0.01405589313879346096 ) ) ;
#3762=CARTESIAN_POINT ( 'NONE',  ( 0.3543307086614173040, 0.2045729300278205931, -0.3766201741223081378 ) ) ;
#3763=CARTESIAN_POINT ( 'NONE',  ( 0.2073490933073314779, -0.2894328052184282352, -3.494844601269712023E-17 ) ) ;
#3772=SHAPE_REPRESENTATION_RELATIONSHIP ( 'NONE' , 'NONE' ,  #5265, #5868 ) ;
#3776=DIRECTION ( 'NONE',  ( 0.000000000000000000, 0.000000000000000000, -1.000000000000000000 ) ) ;
#3786=ORIENTED_EDGE ( 'NONE', *, *, #3941, .T. ) ;
#3799=CARTESIAN_POINT ( 'NONE',  ( -0.3543307086614173040, 0.000000000000000000, 7.886165872636028972E-17 ) ) ;
#3802=CARTESIAN_POINT ( 'NONE',  ( -0.3543307086614173040, -0.03456946083495022332, -0.4082677165354330895 ) ) ;
#3810=DIRECTION ( 'NONE',  ( -0.000000000000000000, -0.000000000000000000, 1.000000000000000000 ) ) ;
#3827=CARTESIAN_POINT ( 'NONE',  ( -0.1171503679538647841, 0.3415090635818126552, -0.003642820150508618762 ) ) ;
#3836=ORIENTED_EDGE ( 'NONE', *, *, #4211, .T. ) ;
#3839=CARTESIAN_POINT ( 'NONE',  ( 0.000000000000000000, 0.000000000000000000, 0.000000000000000000 ) ) ;
#3854=CARTESIAN_POINT ( 'NONE',  ( 0.1771653543307088463, 0.3068593950417300431, 7.886165872636028972E-17 ) ) ;
#3860=DIRECTION ( 'NONE',  ( -0.000000000000000000, -0.000000000000000000, 1.000000000000000000 ) ) ;
#3872=EDGE_LOOP ( 'NONE', ( #1456, #1095, #2410 ) ) ;
#3879=VERTEX_POINT ( 'NONE', #6330 ) ;
#3882=EDGE_CURVE ( 'NONE', #3362, #2406, #7319, .T. ) ;
#3886=CARTESIAN_POINT ( 'NONE',  ( 0.2948818897637794922, 0.000000000000000000, 0.1783464566929134354 ) ) ;
#3897=DIRECTION ( 'NONE',  ( 0.000000000000000000, 0.000000000000000000, -1.000000000000000000 ) ) ;
#3910=DIRECTION ( 'NONE',  ( 1.000000000000000000, 0.000000000000000000, 0.000000000000000000 ) ) ;
#3917=FACE_OUTER_BOUND ( 'NONE', #2126, .T. ) ;
#3918=ORIENTED_EDGE ( 'NONE', *, *, #4860, .F. ) ;
#3921=CARTESIAN_POINT ( 'NONE',  ( -0.1771653543307089018, -0.3068593950417300986, -0.4082677165354330340 ) ) ;
#3941=EDGE_CURVE ( 'NONE', #2077, #1762, #1930, .T. ) ;
#3954=ORIENTED_EDGE ( 'NONE', *, *, #5065, .T. ) ;
#3957=B_SPLINE_CURVE_WITH_KNOTS ( 'NONE', 3,
 ( #3080, #7167, #374, #5080, #1662, #2656 ),
 .UNSPECIFIED., .F., .F.,
 ( 4, 2, 4 ),
 ( 2.380730968228221197E-07, 0.002629065763328360898, 0.005257893453559898435 ),
 .UNSPECIFIED. ) ;
#3971=CIRCLE ( 'NONE', #4687, 0.2066929133858267931 ) ;
#3973=CARTESIAN_POINT ( 'NONE',  ( -0.3543307086614173040, 0.2045729300278199547, -0.03164754241312472960 ) ) ;
#3976=ORIENTED_EDGE ( 'NONE', *, *, #1754, .T. ) ;
#3977=LINE ( 'NONE', #1057, #4922 ) ;
#3982=EDGE_CURVE ( 'NONE', #4654, #3879, #2633, .T. ) ;
#3994=ORIENTED_EDGE ( 'NONE', *, *, #1596, .T. ) ;
#3997=CARTESIAN_POINT ( 'NONE',  ( -0.1771653543307089573, 0.3068593950417301541, 0.000000000000000000 ) ) ;
#3999=VERTEX_POINT ( 'NONE', #6670 ) ;
#4005=CARTESIAN_POINT ( 'NONE',  ( -0.3543307086614173040, 0.1714946277491095350, -0.02209865905065006367 ) ) ;
#4012=VECTOR ( 'NONE', #532, 39.37007874015748143 ) ;
#4017=EDGE_CURVE ( 'NONE', #1108, #4739, #1061, .T. ) ;
#4022=CIRCLE ( 'NONE', #975, 0.3543307086614173596 ) ;
#4028=CARTESIAN_POINT ( 'NONE',  ( 9.857707340795016185E-18, -0.4091458600556410752, -0.4082677165354330340 ) ) ;
#4032=CARTESIAN_POINT ( 'NONE',  ( 0.000000000000000000, 0.000000000000000000, 0.1783464566929134354 ) ) ;
#4049=EDGE_LOOP ( 'NONE', ( #2566, #4354, #4525 ) ) ;
#4059=CARTESIAN_POINT ( 'NONE',  ( -0.3543307086614173040, -0.2045729300278205931, -0.3766201741223081378 ) ) ;
#4062=FACE_OUTER_BOUND ( 'NONE', #3213, .T. ) ;
#4070=CARTESIAN_POINT ( 'NONE',  ( -0.1771653543307089573, 0.3068593950417301541, -0.4082677165354330340 ) ) ;
#4092=CARTESIAN_POINT ( 'NONE',  ( -0.3543307086614173040, -0.03456946083495023719, 4.441920810010739880E-17 ) ) ;
#4096=DIRECTION ( 'NONE',  ( 0.000000000000000000, 0.000000000000000000, 1.000000000000000000 ) ) ;
#4111=ADVANCED_FACE ( 'NONE', ( #3917 ), #6688, .T. ) ;
#4114=CARTESIAN_POINT ( 'NONE',  ( -0.02898191724071506881, -0.3924131423350828429, -0.3862808132025621344 ) ) ;
#4118=AXIS2_PLACEMENT_3D ( 'NONE', #2781, #5006, #6801 ) ;
#4120=ORIENTED_EDGE ( 'NONE', *, *, #6602, .F. ) ;
#4123=ORIENTED_EDGE ( 'NONE', *, *, #4669, .T. ) ;
#4139=VERTEX_POINT ( 'NONE', #2759 ) ;
#4142=AXIS2_PLACEMENT_3D ( 'NONE', #4887, #1906, #5345 ) ;
#4144=EDGE_LOOP ( 'NONE', ( #3671, #6143, #6889 ) ) ;
#4147=CARTESIAN_POINT ( 'NONE',  ( 0.3543307086614173040, 0.06965032677943210071, -0.003053646640237114764 ) ) ;
#4151=CARTESIAN_POINT ( 'NONE',  ( -1.126887297386508504E-15, -0.4091458600556405756, -0.3766201741223081378 ) ) ;
#4154=EDGE_CURVE ( 'NONE', #4931, #4654, #123, .T. ) ;
#4155=EDGE_CURVE ( 'NONE', #1762, #5092, #4784, .T. ) ;
#4165=DIRECTION ( 'NONE',  ( -0.000000000000000000, -0.000000000000000000, 1.000000000000000000 ) ) ;
#4172=VERTEX_POINT ( 'NONE', #4059 ) ;
#4199=CARTESIAN_POINT ( 'NONE',  ( 0.000000000000000000, 0.000000000000000000, -0.4082677165354330340 ) ) ;
#4205=CARTESIAN_POINT ( 'NONE',  ( -0.2362204724409449619, 0.000000000000000000, -0.4072677165354330331 ) ) ;
#4211=EDGE_CURVE ( 'NONE', #7286, #5092, #6811, .T. ) ;
#4215=B_SPLINE_CURVE_WITH_KNOTS ( 'NONE', 3,
 ( #4070, #2875, #497, #3428, #7502, #2272, #6400, #1144 ),
 .UNSPECIFIED., .F., .F.,
 ( 4, 2, 2, 4 ),
 ( 0.005257893453559884557, 0.006567392922673222569, 0.007876892391786559713, 0.01049589133001323574 ),
 .UNSPECIFIED. ) ;
#4216=EDGE_CURVE ( 'NONE', #1378, #5614, #1550, .T. ) ;
#4221=CARTESIAN_POINT ( 'NONE',  ( -0.2371576072764295939, 0.2722228516542259391, -0.4052515342986937608 ) ) ;
#4225=VERTEX_POINT ( 'NONE', #7118 ) ;
#4227=( LENGTH_UNIT ( ) NAMED_UNIT ( * ) SI_UNIT ( $, .METRE. ) );
#4229=DIRECTION ( 'NONE',  ( -1.000000000000000000, 0.000000000000000000, 0.000000000000000000 ) ) ;
#4235=CARTESIAN_POINT ( 'NONE',  ( 0.000000000000000000, 0.000000000000000000, -0.4082677165354330340 ) ) ;
#4240=DIRECTION ( 'NONE',  ( -0.5000000000000008882, 0.8660254037844381525, 0.000000000000000000 ) ) ;
#4250=AXIS2_PLACEMENT_3D ( 'NONE', #7409, #2749, #5639 ) ;
#4262=ORIENTED_EDGE ( 'NONE', *, *, #6957, .F. ) ;
#4271=CARTESIAN_POINT ( 'NONE',  ( 3.414809992080329023E-17, 0.4091458600556405201, -0.03164754241312491001 ) ) ;
#4273=CARTESIAN_POINT ( 'NONE',  ( 0.000000000000000000, 0.000000000000000000, 0.000000000000000000 ) ) ;
#4274=CARTESIAN_POINT ( 'NONE',  ( -0.3254211578371894453, -0.2212638669783398016, -0.02201102547170743703 ) ) ;
#4275=CARTESIAN_POINT ( 'NONE',  ( 0.3543307086614173596, -0.1713008003332313622, -0.3862250106401512451 ) ) ;
#4279=DIRECTION ( 'NONE',  ( 0.000000000000000000, 0.000000000000000000, 1.000000000000000000 ) ) ;
#4296=CIRCLE ( 'NONE', #3446, 0.2066929133858267931 ) ;
#4298=EDGE_LOOP ( 'NONE', ( #3786, #934, #4700 ) ) ;
#4299=CARTESIAN_POINT ( 'NONE',  ( 0.000000000000000000, 0.000000000000000000, 0.1783464566929134354 ) ) ;
#4306=( NAMED_UNIT ( * ) SI_UNIT ( $, .STERADIAN. ) SOLID_ANGLE_UNIT ( ) );
#4308=DIRECTION ( 'NONE',  ( 0.8191520442889907994, 1.003171929053523514E-16, -0.5735764363510474917 ) ) ;
#4309=DIRECTION ( 'NONE',  ( 1.000000000000000000, 0.000000000000000000, 0.000000000000000000 ) ) ;
#4342=DIRECTION ( 'NONE',  ( 1.000000000000000000, 0.000000000000000000, 0.000000000000000000 ) ) ;
#4349=DIRECTION ( 'NONE',  ( -1.000000000000000000, 0.000000000000000000, -0.000000000000000000 ) ) ;
#4354=ORIENTED_EDGE ( 'NONE', *, *, #6966, .T. ) ;
#4365=ORIENTED_EDGE ( 'NONE', *, *, #4718, .F. ) ;
#4391=LINE ( 'NONE', #6686, #2291 ) ;
#4392=DIRECTION ( 'NONE',  ( -0.000000000000000000, -0.000000000000000000, 1.000000000000000000 ) ) ;
#4402=CARTESIAN_POINT ( 'NONE',  ( 3.414809992080329023E-17, 0.4091458600556405201, -0.03164754241312491001 ) ) ;
#4408=DIRECTION ( 'NONE',  ( -0.000000000000000000, -0.000000000000000000, 1.000000000000000000 ) ) ;
#4410=VERTEX_POINT ( 'NONE', #4402 ) ;
#4411=AXIS2_PLACEMENT_3D ( 'NONE', #611, #6580, #2400 ) ;
#4416=ORIENTED_EDGE ( 'NONE', *, *, #6446, .T. ) ;
#4420=DIRECTION ( 'NONE',  ( 1.000000000000000000, 0.000000000000000000, 0.000000000000000000 ) ) ;
#4434=FACE_OUTER_BOUND ( 'NONE', #357, .T. ) ;
#4436=AXIS2_PLACEMENT_3D ( 'NONE', #5059, #1562, #3910 ) ;
#4443=CARTESIAN_POINT ( 'NONE',  ( 0.2371803407075527004, 0.2722097265016475420, -0.003642820150508603583 ) ) ;
#4459=CARTESIAN_POINT ( 'NONE',  ( 0.3543307086614172485, 0.000000000000000000, 0.3732633159281743551 ) ) ;
#4462=EDGE_CURVE ( 'NONE', #1296, #1000, #4551, .T. ) ;
#4466=LINE ( 'NONE', #2653, #5991 ) ;
#4467=CARTESIAN_POINT ( 'NONE',  ( -0.3543307086614173040, 0.1379824317933223410, -0.3941213672119904809 ) ) ;
#4486=ADVANCED_FACE ( 'NONE', ( #1675 ), #5745, .T. ) ;
#4500=DIRECTION ( 'NONE',  ( 1.224646799147353207E-16, 1.000000000000000000, 0.000000000000000000 ) ) ;
#4511=EDGE_LOOP ( 'NONE', ( #2523, #2868, #404, #884 ) ) ;
#4512=CIRCLE ( 'NONE', #3408, 0.3543307086614173596 ) ;
#4514=CARTESIAN_POINT ( 'NONE',  ( 0.2371803407075526726, 0.2722097265016474310, -0.4046248963849245484 ) ) ;
#4525=ORIENTED_EDGE ( 'NONE', *, *, #4462, .F. ) ;
#4530=ORIENTED_EDGE ( 'NONE', *, *, #488, .T. ) ;
#4551=B_SPLINE_CURVE_WITH_KNOTS ( 'NONE', 3,
 ( #5056, #3286, #959, #4443, #3365, #7333, #1062, #433 ),
 .UNSPECIFIED., .F., .F.,
 ( 4, 2, 2, 4 ),
 ( 0.005257893453559899302, 0.006567392922673231243, 0.007876892391786563183, 0.01049589133001322706 ),
 .UNSPECIFIED. ) ;
#4562=CARTESIAN_POINT ( 'NONE',  ( -0.3253487914207032206, 0.2213056477483777151, -0.02198690333287076776 ) ) ;
#4567=CARTESIAN_POINT ( 'NONE',  ( -0.2962704110120346623, -0.2380940585049214631, -0.3942118233966396268 ) ) ;
#4589=DIRECTION ( 'NONE',  ( -1.000000000000000000, -3.552713678800500929E-15, 0.000000000000000000 ) ) ;
#4596=B_SPLINE_CURVE_WITH_KNOTS ( 'NONE', 3,
 ( #5253, #6559, #3605, #4221, #5830, #2454 ),
 .UNSPECIFIED., .F., .F.,
 ( 4, 2, 4 ),
 ( 2.380730968297687428E-07, 0.002629065763328357428, 0.005257893453559884557 ),
 .UNSPECIFIED. ) ;
#4604=ORIENTED_EDGE ( 'NONE', *, *, #5904, .F. ) ;
#4622=DIRECTION ( 'NONE',  ( -0.000000000000000000, -0.000000000000000000, 1.000000000000000000 ) ) ;
#4627=ORIENTED_EDGE ( 'NONE', *, *, #4017, .F. ) ;
#4630=ADVANCED_FACE ( 'NONE', ( #685 ), #5609, .T. ) ;
#4633=FACE_OUTER_BOUND ( 'NONE', #2803, .T. ) ;
#4645=CARTESIAN_POINT ( 'NONE',  ( 0.2362204724409449619, 0.000000000000000000, -0.4082677165354330340 ) ) ;
#4650=CARTESIAN_POINT ( 'NONE',  ( 0.3543307086614172485, 0.000000000000000000, 0.1188976377952756375 ) ) ;
#4654=VERTEX_POINT ( 'NONE', #1907 ) ;
#4660=CARTESIAN_POINT ( 'NONE',  ( 0.000000000000000000, 0.000000000000000000, 0.000000000000000000 ) ) ;
#4669=EDGE_CURVE ( 'NONE', #5183, #1296, #2895, .T. ) ;
#4672=CARTESIAN_POINT ( 'NONE',  ( 0.000000000000000000, 0.000000000000000000, 0.1783464566929134354 ) ) ;
#4673=DIRECTION ( 'NONE',  ( -1.000000000000000000, 3.552713678800500929E-15, 0.000000000000000000 ) ) ;
#4676=EDGE_CURVE ( 'NONE', #2077, #2074, #5675, .T. ) ;
#4687=AXIS2_PLACEMENT_3D ( 'NONE', #1048, #410, #791 ) ;
#4700=ORIENTED_EDGE ( 'NONE', *, *, #4676, .F. ) ;
#4718=EDGE_CURVE ( 'NONE', #929, #1000, #4391, .T. ) ;
#4739=VERTEX_POINT ( 'NONE', #4846 ) ;
#4746=EDGE_LOOP ( 'NONE', ( #6418, #6963, #7126, #2497, #3549, #2756 ) ) ;
#4747=DIRECTION ( 'NONE',  ( -0.000000000000000000, -0.000000000000000000, 1.000000000000000000 ) ) ;
#4758=CARTESIAN_POINT ( 'NONE',  ( 0.2699662542182227343, 0.000000000000000000, 0.1783464566929134354 ) ) ;
#4771=CIRCLE ( 'NONE', #7451, 0.2948818897637794922 ) ;
#4775=DIRECTION ( 'NONE',  ( -0.8660254037844380415, -0.5000000000000007772, 0.000000000000000000 ) ) ;
#4780=CARTESIAN_POINT ( 'NONE',  ( 0.000000000000000000, 0.000000000000000000, 0.1188976377952756375 ) ) ;
#4783=CARTESIAN_POINT ( 'NONE',  ( 0.05806029764938262783, -0.3756247315785400387, -0.01405589313879368647 ) ) ;
#4784=LINE ( 'NONE', #5900, #6934 ) ;
#4789=VECTOR ( 'NONE', #11, 39.37007874015748143 ) ;
#4797=DIRECTION ( 'NONE',  ( 1.000000000000000000, 0.000000000000000000, 0.000000000000000000 ) ) ;
#4800=AXIS2_PLACEMENT_3D ( 'NONE', #3206, #6160, #5514 ) ;
#4804=CONICAL_SURFACE ( 'NONE', #3576, 0.3543307086614173596, 1.047197551196596521 ) ;
#4805=CARTESIAN_POINT ( 'NONE',  ( 0.3543307086614173040, 0.2045729300278205931, -0.03164754241312491001 ) ) ;
#4826=ORIENTED_EDGE ( 'NONE', *, *, #6184, .T. ) ;
#4835=ORIENTED_EDGE ( 'NONE', *, *, #979, .T. ) ;
#4843=FACE_OUTER_BOUND ( 'NONE', #5111, .T. ) ;
#4846=CARTESIAN_POINT ( 'NONE',  ( 0.2066929133858267931, 0.000000000000000000, 0.1188976377952756375 ) ) ;
#4855=CARTESIAN_POINT ( 'NONE',  ( 0.1771653543307088463, -0.3068593950417300431, 7.886165872636028972E-17 ) ) ;
#4860=EDGE_CURVE ( 'NONE', #4225, #2266, #3149, .T. ) ;
#4864=DIRECTION ( 'NONE',  ( -0.000000000000000000, -0.000000000000000000, 1.000000000000000000 ) ) ;
#4867=EDGE_CURVE ( 'NONE', #6033, #3513, #5114, .T. ) ;
#4871=DIRECTION ( 'NONE',  ( -0.000000000000000000, 0.000000000000000000, -1.000000000000000000 ) ) ;
#4877=AXIS2_PLACEMENT_3D ( 'NONE', #5256, #3897, #6800 ) ;
#4887=CARTESIAN_POINT ( 'NONE',  ( 0.000000000000000000, 0.000000000000000000, -0.4082677165354330340 ) ) ;
#4896=AXIS2_PLACEMENT_3D ( 'NONE', #3128, #197, #2031 ) ;
#4902=ORIENTED_EDGE ( 'NONE', *, *, #3321, .T. ) ;
#4909=ORIENTED_EDGE ( 'NONE', *, *, #1438, .T. ) ;
#4911=CARTESIAN_POINT ( 'NONE',  ( -0.3543307086614173596, -0.1713008003332314177, -0.3862250106401512451 ) ) ;
#4914=CARTESIAN_POINT ( 'NONE',  ( -0.3543307086614173040, 0.2045729300278205931, -0.3766201741223081378 ) ) ;
#4922=VECTOR ( 'NONE', #2816, 39.37007874015748143 ) ;
#4931=VERTEX_POINT ( 'NONE', #1810 ) ;
#4950=LINE ( 'NONE', #3147, #6700 ) ;
#4959=CARTESIAN_POINT ( 'NONE',  ( 0.000000000000000000, 0.000000000000000000, -0.4072677165354330331 ) ) ;
#4972=APPLICATION_CONTEXT ( 'automotive_design' ) ;
#4973=ORIENTED_EDGE ( 'NONE', *, *, #5286, .T. ) ;
#4979=ORIENTED_EDGE ( 'NONE', *, *, #2320, .F. ) ;
#4991=CARTESIAN_POINT ( 'NONE',  ( 0.2362204724409449619, 2.892866454678788147E-17, -0.4072677165354330331 ) ) ;
#4996=DIRECTION ( 'NONE',  ( -0.000000000000000000, -0.000000000000000000, 1.000000000000000000 ) ) ;
#5006=DIRECTION ( 'NONE',  ( 0.000000000000000000, -0.000000000000000000, 1.000000000000000000 ) ) ;
#5007=CARTESIAN_POINT ( 'NONE',  ( 0.000000000000000000, 0.000000000000000000, 0.1188976377952756375 ) ) ;
#5022=CARTESIAN_POINT ( 'NONE',  ( 0.000000000000000000, 0.000000000000000000, 0.1783464566929134354 ) ) ;
#5042=AXIS2_PLACEMENT_3D ( 'NONE', #2911, #2844, #5915 ) ;
#5056=CARTESIAN_POINT ( 'NONE',  ( 0.1771653543307088463, 0.3068593950417300431, 7.886165872636028972E-17 ) ) ;
#5059=CARTESIAN_POINT ( 'NONE',  ( 0.000000000000000000, 0.000000000000000000, -0.9857285720115422922 ) ) ;
#5065=EDGE_CURVE ( 'NONE', #5707, #6705, #2115, .T. ) ;
#5073=ORIENTED_EDGE ( 'NONE', *, *, #3070, .T. ) ;
#5080=CARTESIAN_POINT ( 'NONE',  ( 0.1171731013849879183, 0.3414959384292343136, -0.4052515342986937608 ) ) ;
#5082=CARTESIAN_POINT ( 'NONE',  ( 0.1171731013849879460, 0.3414959384292343136, -0.003016182236739221607 ) ) ;
#5092=VERTEX_POINT ( 'NONE', #6211 ) ;
#5100=EDGE_CURVE ( 'NONE', #662, #7286, #292, .T. ) ;
#5109=EDGE_CURVE ( 'NONE', #4172, #5128, #7386, .T. ) ;
#5111=EDGE_LOOP ( 'NONE', ( #2942, #3569 ) ) ;
#5114=CIRCLE ( 'NONE', #1612, 0.2699662542182227343 ) ;
#5119=CONICAL_SURFACE ( 'NONE', #7055, 0.3543307086614173596, 1.047197551196596521 ) ;
#5120=CARTESIAN_POINT ( 'NONE',  ( 0.1469816153540864645, 0.3242859848650326282, 2.518422369159242870E-16 ) ) ;
#5127=CARTESIAN_POINT ( 'NONE',  ( -0.2699662542182227343, 3.306133091061471023E-17, 0.1188976377952756375 ) ) ;
#5128=VERTEX_POINT ( 'NONE', #1968 ) ;
#5134=ORIENTED_EDGE ( 'NONE', *, *, #701, .T. ) ;
#5148=CYLINDRICAL_SURFACE ( 'NONE', #7225, 0.2362204724409449619 ) ;
#5157=CARTESIAN_POINT ( 'NONE',  ( -0.3543307086614173040, -0.2045729300278205653, -0.4082677165354330340 ) ) ;
#5160=VECTOR ( 'NONE', #5267, 39.37007874015748143 ) ;
#5163=ADVANCED_FACE ( 'NONE', ( #2299 ), #5148, .F. ) ;
#5166=AXIS2_PLACEMENT_3D ( 'NONE', #418, #2134, #2741 ) ;
#5167=DIRECTION ( 'NONE',  ( 1.000000000000000000, 0.000000000000000000, 0.000000000000000000 ) ) ;
#5168=AXIS2_PLACEMENT_3D ( 'NONE', #2189, #1488, #5566 ) ;
#5170=AXIS2_PLACEMENT_3D ( 'NONE', #2428, #6909, #2611 ) ;
#5174=ORIENTED_EDGE ( 'NONE', *, *, #1199, .F. ) ;
#5179=AXIS2_PLACEMENT_3D ( 'NONE', #6681, #261, #2622 ) ;
#5183=VERTEX_POINT ( 'NONE', #3997 ) ;
#5186=CARTESIAN_POINT ( 'NONE',  ( -0.3543307086614173040, -0.2045729300278205931, -0.3766201741223081378 ) ) ;
#5190=DIRECTION ( 'NONE',  ( 1.000000000000000000, 0.000000000000000000, 0.000000000000000000 ) ) ;
#5194=CARTESIAN_POINT ( 'NONE',  ( -0.3543307086614173040, 0.1379824317933219802, -0.01414634932344258599 ) ) ;
#5201=FACE_BOUND ( 'NONE', #3263, .T. ) ;
#5219=B_SPLINE_CURVE_WITH_KNOTS ( 'NONE', 3,
 ( #7291, #2069, #1474, #3827, #6161, #5777, #3436, #1092 ),
 .UNSPECIFIED., .F., .F.,
 ( 4, 2, 2, 4 ),
 ( 0.005257893453559884557, 0.006567392922673222569, 0.007876892391786559713, 0.01049589133001323574 ),
 .UNSPECIFIED. ) ;
#5229=ADVANCED_FACE ( 'NONE', ( #4633 ), #3202, .T. ) ;
#5242=EDGE_CURVE ( 'NONE', #4225, #4172, #6757, .T. ) ;
#5248=CARTESIAN_POINT ( 'NONE',  ( -0.3543307086614173040, 0.000000000000000000, 7.886165872636028972E-17 ) ) ;
#5253=CARTESIAN_POINT ( 'NONE',  ( -0.3543307086614173040, 0.2045729300278205931, -0.3766201741223081378 ) ) ;
#5256=CARTESIAN_POINT ( 'NONE',  ( -6.829619984160658046E-17, 0.4091458600556405201, -0.4082677165354330340 ) ) ;
#5257=DIRECTION ( 'NONE',  ( -0.000000000000000000, -0.000000000000000000, 1.000000000000000000 ) ) ;
#5258=ORIENTED_EDGE ( 'NONE', *, *, #4462, .T. ) ;
#5265=SHAPE_REPRESENTATION ( 'torque nut 09_iso_ISO 10512-M12x1.5-N', ( #5166 ), #6134 ) ;
#5267=DIRECTION ( 'NONE',  ( -0.000000000000000000, -0.000000000000000000, 1.000000000000000000 ) ) ;
#5271=FACE_OUTER_BOUND ( 'NONE', #4144, .T. ) ;
#5286=EDGE_CURVE ( 'NONE', #2074, #1762, #3655, .T. ) ;
#5292=CARTESIAN_POINT ( 'NONE',  ( 0.3543307086614173040, 0.06965032677943194805, -0.4052140698951960385 ) ) ;
#5318=CARTESIAN_POINT ( 'NONE',  ( 0.000000000000000000, 0.000000000000000000, -0.4082677165354330340 ) ) ;
#5321=PRODUCT ( 'torque nut 09_iso_ISO 10512-M12x1.5-N', 'torque nut 09_iso_ISO 10512-M12x1.5-N', '', ( #5908 ) ) ;
#5328=FACE_OUTER_BOUND ( 'NONE', #1047, .T. ) ;
#5332=CYLINDRICAL_SURFACE ( 'NONE', #2105, 0.3543307086614172485 ) ;
#5334=EDGE_CURVE ( 'NONE', #5614, #1378, #164, .T. ) ;
#5339=AXIS2_PLACEMENT_3D ( 'NONE', #856, #4408, #6065 ) ;
#5342=CARTESIAN_POINT ( 'NONE',  ( 0.2362204724409449619, 0.000000000000000000, -0.9857285720115422922 ) ) ;
#5345=DIRECTION ( 'NONE',  ( -1.000000000000000000, 1.776356839400250465E-15, 0.000000000000000000 ) ) ;
#5355=CARTESIAN_POINT ( 'NONE',  ( 0.1470270249832138776, -0.3242597676034325582, -0.0007480297793126593165 ) ) ;
#5357=DIRECTION ( 'NONE',  ( -1.000000000000000000, 0.000000000000000000, 0.000000000000000000 ) ) ;
#5362=ORIENTED_EDGE ( 'NONE', *, *, #3542, .F. ) ;
#5373=DIRECTION ( 'NONE',  ( -0.000000000000000000, 0.000000000000000000, -1.000000000000000000 ) ) ;
#5389=( GEOMETRIC_REPRESENTATION_CONTEXT ( 3 ) GLOBAL_UNCERTAINTY_ASSIGNED_CONTEXT ( ( #1849 ) ) GLOBAL_UNIT_ASSIGNED_CONTEXT ( ( #3109, #1418, #3651 ) ) REPRESENTATION_CONTEXT ( 'NONE', 'WORKASPACE' ) );
#5390=DIRECTION ( 'NONE',  ( 0.000000000000000000, 0.000000000000000000, -1.000000000000000000 ) ) ;
#5393=CARTESIAN_POINT ( 'NONE',  ( 0.3543307086614173596, 0.000000000000000000, -0.4082677165354330340 ) ) ;
#5402=CARTESIAN_POINT ( 'NONE',  ( 0.02890955082422775116, -0.3924549231051219778, -0.02201102547170776663 ) ) ;
#5435=DIRECTION ( 'NONE',  ( 0.000000000000000000, 0.000000000000000000, 1.000000000000000000 ) ) ;
#5441=CARTESIAN_POINT ( 'NONE',  ( 6.901988839087968355E-18, 0.4091458600556405201, -0.4082677165354330340 ) ) ;
#5457=DIRECTION ( 'NONE',  ( 0.000000000000000000, 0.000000000000000000, 1.000000000000000000 ) ) ;
#5473=ORIENTED_EDGE ( 'NONE', *, *, #2320, .T. ) ;
#5474=AXIS2_PLACEMENT_3D ( 'NONE', #288, #4871, #778 ) ;
#5477=CARTESIAN_POINT ( 'NONE',  ( 0.2371576072764297882, -0.2722228516542265497, -0.4052515342986934832 ) ) ;
#5478=EDGE_CURVE ( 'NONE', #6455, #4139, #2238, .T. ) ;
#5486=ORIENTED_EDGE ( 'NONE', *, *, #4867, .F. ) ;
#5495=CARTESIAN_POINT ( 'NONE',  ( -0.1469816153540868531, -0.3242859848650329058, -2.174273549644897140E-17 ) ) ;
#5499=CARTESIAN_POINT ( 'NONE',  ( 9.857707340795016185E-18, -0.4091458600556410752, -0.4082677165354330340 ) ) ;
#5512=CARTESIAN_POINT ( 'NONE',  ( -0.1771653543307088186, -0.3068593950417299876, 7.886165872636028972E-17 ) ) ;
#5514=DIRECTION ( 'NONE',  ( 0.000000000000000000, 0.000000000000000000, 1.000000000000000000 ) ) ;
#5525=CIRCLE ( 'NONE', #6488, 0.3543307086614173596 ) ;
#5538=AXIS2_PLACEMENT_3D ( 'NONE', #1262, #4747, #7080 ) ;
#5548=AXIS2_PLACEMENT_3D ( 'NONE', #600, #5807, #6375 ) ;
#5563=ORIENTED_EDGE ( 'NONE', *, *, #5109, .T. ) ;
#5566=DIRECTION ( 'NONE',  ( 0.000000000000000000, 0.000000000000000000, -1.000000000000000000 ) ) ;
#5573=ADVANCED_FACE ( 'NONE', ( #3443 ), #1645, .F. ) ;
#5575=ADVANCED_FACE ( 'NONE', ( #3407 ), #7448, .F. ) ;
#5609=CONICAL_SURFACE ( 'NONE', #6695, 0.3543307086614173596, 1.047197551196596521 ) ;
#5611=VERTEX_POINT ( 'NONE', #1066 ) ;
#5614=VERTEX_POINT ( 'NONE', #5749 ) ;
#5627=CARTESIAN_POINT ( 'NONE',  ( 0.1771653543307088463, 0.3068593950417300431, 7.886165872636028972E-17 ) ) ;
#5636=ORIENTED_EDGE ( 'NONE', *, *, #340, .F. ) ;
#5639=DIRECTION ( 'NONE',  ( 0.8660254037844382635, -0.5000000000000005551, 0.000000000000000000 ) ) ;
#5641=LINE ( 'NONE', #6954, #493 ) ;
#5649=AXIS2_PLACEMENT_3D ( 'NONE', #430, #1555, #1673 ) ;
#5660=AXIS2_PLACEMENT_3D ( 'NONE', #5318, #171, #5980 ) ;
#5674=PLANE ( 'NONE',  #5649 ) ;
#5675=B_SPLINE_CURVE_WITH_KNOTS ( 'NONE', 3,
 ( #6613, #1322, #3668, #3165, #1398, #3743, #4274, #6007 ),
 .UNSPECIFIED., .F., .F.,
 ( 4, 2, 2, 4 ),
 ( 0.005257893453559907976, 0.006567392922673238181, 0.007876892391786568387, 0.01049589133001323227 ),
 .UNSPECIFIED. ) ;
#5683=B_SPLINE_CURVE_WITH_KNOTS ( 'NONE', 3,
 ( #7444, #2713, #6915, #4514, #7407, #7482, #5709, #541 ),
 .UNSPECIFIED., .F., .F.,
 ( 4, 2, 2, 4 ),
 ( 0.005257893453559898435, 0.006567392922673230375, 0.007876892391786563183, 0.01049589133001322706 ),
 .UNSPECIFIED. ) ;
#5692=CARTESIAN_POINT ( 'NONE',  ( -0.2073036836782042036, -0.2894590224800286937, -0.4075196867561204361 ) ) ;
#5693=CIRCLE ( 'NONE', #3352, 0.2699662542182227343 ) ;
#5707=VERTEX_POINT ( 'NONE', #4205 ) ;
#5709=CARTESIAN_POINT ( 'NONE',  ( 0.3254211578371891678, 0.2212638669783393297, -0.3862566910637258433 ) ) ;
#5711=ORIENTED_EDGE ( 'NONE', *, *, #2479, .T. ) ;
#5712=DIMENSIONAL_EXPONENTS ( 1.000000000000000000, 0.000000000000000000, 0.000000000000000000, 0.000000000000000000, 0.000000000000000000, 0.000000000000000000, 0.000000000000000000 ) ;
#5715=CARTESIAN_POINT ( 'NONE',  ( 0.000000000000000000, 0.000000000000000000, -0.4082677165354330340 ) ) ;
#5716=ADVANCED_FACE ( 'NONE', ( #5271 ), #6512, .T. ) ;
#5719=CARTESIAN_POINT ( 'NONE',  ( -0.2371576072764296494, 0.2722228516542259946, -0.003016182236739215101 ) ) ;
#5722=ORIENTED_EDGE ( 'NONE', *, *, #3321, .F. ) ;
#5739=DIRECTION ( 'NONE',  ( -0.8191520442889907994, 0.000000000000000000, -0.5735764363510474917 ) ) ;
#5740=CARTESIAN_POINT ( 'NONE',  ( 0.000000000000000000, 0.000000000000000000, 0.1188976377952756375 ) ) ;
#5745=PLANE ( 'NONE',  #4250 ) ;
#5749=CARTESIAN_POINT ( 'NONE',  ( -0.2362204724409449619, 2.892866454678788147E-17, -0.4082677165354330340 ) ) ;
#5750=ORIENTED_EDGE ( 'NONE', *, *, #2059, .F. ) ;
#5767=B_SPLINE_CURVE_WITH_KNOTS ( 'NONE', 3,
 ( #4151, #4114, #681, #2920, #3541, #717 ),
 .UNSPECIFIED., .F., .F.,
 ( 4, 2, 4 ),
 ( 2.380730968541169696E-07, 0.002629065763328381714, 0.005257893453559908843 ),
 .UNSPECIFIED. ) ;
#5777=CARTESIAN_POINT ( 'NONE',  ( -0.05806029764938282212, 0.3756247315785394836, -0.01405589313879331177 ) ) ;
#5790=DIRECTION ( 'NONE',  ( 1.000000000000000000, 0.000000000000000000, 0.000000000000000000 ) ) ;
#5798=DIRECTION ( 'NONE',  ( 1.000000000000000000, 0.000000000000000000, 0.000000000000000000 ) ) ;
#5800=CARTESIAN_POINT ( 'NONE',  ( 0.000000000000000000, 0.000000000000000000, 0.3732633159281743551 ) ) ;
#5802=ADVANCED_FACE ( 'NONE', ( #233 ), #3712, .T. ) ;
#5807=DIRECTION ( 'NONE',  ( 0.000000000000000000, 0.000000000000000000, -1.000000000000000000 ) ) ;
#5830=CARTESIAN_POINT ( 'NONE',  ( -0.2073490933073312281, 0.2894328052184277356, -0.4082677165354333115 ) ) ;
#5855=CARTESIAN_POINT ( 'NONE',  ( -0.3543307086614173040, 0.2045729300278199547, -0.03164754241312472960 ) ) ;
#5856=AXIS2_PLACEMENT_3D ( 'NONE', #4028, #2300, #622 ) ;
#5868=ADVANCED_BREP_SHAPE_REPRESENTATION ( '', ( #6540, #5166 ), #6134 ) ;
#5869=DIRECTION ( 'NONE',  ( 1.000000000000000000, 0.000000000000000000, 0.000000000000000000 ) ) ;
#5871=AXIS2_PLACEMENT_3D ( 'NONE', #4780, #4165, #6504 ) ;
#5878=EDGE_CURVE ( 'NONE', #2266, #1419, #498, .T. ) ;
#5881=LINE ( 'NONE', #5342, #5160 ) ;
#5894=CIRCLE ( 'NONE', #166, 0.3543307086614173596 ) ;
#5900=CARTESIAN_POINT ( 'NONE',  ( -0.3543307086614172485, 4.339299682018179447E-17, 0.3732633159281743551 ) ) ;
#5904=EDGE_CURVE ( 'NONE', #1068, #1108, #3977, .T. ) ;
#5908=PRODUCT_CONTEXT ( 'NONE', #2474, 'mechanical' ) ;
#5913=EDGE_LOOP ( 'NONE', ( #5486, #5473, #969, #3190 ) ) ;
#5915=DIRECTION ( 'NONE',  ( 1.000000000000000000, 0.000000000000000000, 0.000000000000000000 ) ) ;
#5918=CARTESIAN_POINT ( 'NONE',  ( 0.3543307086614173596, 0.03458999977076016724, 3.421479542846110323E-17 ) ) ;
#5926=DIRECTION ( 'NONE',  ( -0.000000000000000000, -0.000000000000000000, 1.000000000000000000 ) ) ;
#5930=CARTESIAN_POINT ( 'NONE',  ( 0.3543307086614173040, -0.06891495372886456694, -0.4052962681128434164 ) ) ;
#5937=CARTESIAN_POINT ( 'NONE',  ( 0.1023119647485438155, -0.3500760196667496715, -0.005786797686151859930 ) ) ;
#5943=CARTESIAN_POINT ( 'NONE',  ( 0.000000000000000000, 0.000000000000000000, -0.4082677165354330340 ) ) ;
#5945=EDGE_LOOP ( 'NONE', ( #3609, #1933, #5174, #7149, #2649, #3918 ) ) ;
#5978=ORIENTED_EDGE ( 'NONE', *, *, #7152, .F. ) ;
#5980=DIRECTION ( 'NONE',  ( -1.000000000000000000, 0.000000000000000000, 0.000000000000000000 ) ) ;
#5990=DIRECTION ( 'NONE',  ( 0.000000000000000000, 0.000000000000000000, 1.000000000000000000 ) ) ;
#5991=VECTOR ( 'NONE', #4308, 39.37007874015748143 ) ;
#6003=PLANE ( 'NONE',  #1346 ) ;
#6007=CARTESIAN_POINT ( 'NONE',  ( -0.3543307086614173040, -0.2045729300278205931, -0.03164754241312491001 ) ) ;
#6008=LINE ( 'NONE', #7175, #1563 ) ;
#6023=AXIS2_PLACEMENT_3D ( 'NONE', #6860, #2802, #523 ) ;
#6033=VERTEX_POINT ( 'NONE', #5127 ) ;
#6038=ADVANCED_FACE ( 'NONE', ( #4434 ), #4804, .T. ) ;
#6046=ADVANCED_FACE ( 'NONE', ( #2312 ), #6133, .F. ) ;
#6065=DIRECTION ( 'NONE',  ( 1.000000000000000000, 0.000000000000000000, 0.000000000000000000 ) ) ;
#6071=EDGE_LOOP ( 'NONE', ( #6748, #2288, #5258, #4365, #5978, #3728 ) ) ;
#6077=ADVANCED_FACE ( 'NONE', ( #3003 ), #7239, .T. ) ;
#6083=PLANE ( 'NONE',  #594 ) ;
#6097=ORIENTED_EDGE ( 'NONE', *, *, #5242, .F. ) ;
#6098=ORIENTED_EDGE ( 'NONE', *, *, #1731, .F. ) ;
#6107=CARTESIAN_POINT ( 'NONE',  ( 0.2699662542182227343, 0.000000000000000000, 0.1188976377952756375 ) ) ;
#6109=AXIS2_PLACEMENT_3D ( 'NONE', #259, #6793, #336 ) ;
#6128=ORIENTED_EDGE ( 'NONE', *, *, #5334, .F. ) ;
#6133=CONICAL_SURFACE ( 'NONE', #5548, 0.2362204724409449619, 0.9599310885968795892 ) ;
#6134=( GEOMETRIC_REPRESENTATION_CONTEXT ( 3 ) GLOBAL_UNCERTAINTY_ASSIGNED_CONTEXT ( ( #224 ) ) GLOBAL_UNIT_ASSIGNED_CONTEXT ( ( #1420, #2618, #4306 ) ) REPRESENTATION_CONTEXT ( 'NONE', 'WORKASPACE' ) );
#6143=ORIENTED_EDGE ( 'NONE', *, *, #7005, .T. ) ;
#6145=ORIENTED_EDGE ( 'NONE', *, *, #2769, .F. ) ;
#6160=DIRECTION ( 'NONE',  ( -1.000000000000000000, 0.000000000000000000, 0.000000000000000000 ) ) ;
#6161=CARTESIAN_POINT ( 'NONE',  ( -0.1023119647485438294, 0.3500760196667492274, -0.005786797686151529466 ) ) ;
#6170=DIRECTION ( 'NONE',  ( -1.000000000000000000, 0.000000000000000000, 0.000000000000000000 ) ) ;
#6184=EDGE_CURVE ( 'NONE', #3879, #2077, #898, .T. ) ;
#6193=DIRECTION ( 'NONE',  ( 1.000000000000000000, 0.000000000000000000, 0.000000000000000000 ) ) ;
#6200=DIRECTION ( 'NONE',  ( -0.000000000000000000, -0.000000000000000000, 1.000000000000000000 ) ) ;
#6211=CARTESIAN_POINT ( 'NONE',  ( -0.3543307086614172485, 4.339299682018179447E-17, 0.1188976377952756375 ) ) ;
#6219=CARTESIAN_POINT ( 'NONE',  ( 0.000000000000000000, 0.000000000000000000, 0.000000000000000000 ) ) ;
#6220=AXIS2_PLACEMENT_3D ( 'NONE', #392, #6200, #3288 ) ;
#6222=ADVANCED_FACE ( 'NONE', ( #1423 ), #1872, .F. ) ;
#6232=CARTESIAN_POINT ( 'NONE',  ( 0.05806029764938244742, -0.3756247315785402607, -0.3942118233966392382 ) ) ;
#6241=ORIENTED_EDGE ( 'NONE', *, *, #6926, .F. ) ;
#6257=CARTESIAN_POINT ( 'NONE',  ( -0.2948818897637794367, 3.611261624257350948E-17, 0.1188976377952756375 ) ) ;
#6269=AXIS2_PLACEMENT_3D ( 'NONE', #4959, #3776, #3736 ) ;
#6273=EDGE_CURVE ( 'NONE', #3631, #5611, #3957, .T. ) ;
#6304=DIRECTION ( 'NONE',  ( -0.000000000000000000, -0.000000000000000000, 1.000000000000000000 ) ) ;
#6305=CARTESIAN_POINT ( 'NONE',  ( 0.02890955082422759503, -0.3924549231051219222, -0.3862566910637251216 ) ) ;
#6317=ORIENTED_EDGE ( 'NONE', *, *, #6966, .F. ) ;
#6320=EDGE_CURVE ( 'NONE', #5128, #6553, #2843, .T. ) ;
#6330=CARTESIAN_POINT ( 'NONE',  ( 0.1771653543307088463, -0.3068593950417300431, 7.886165872636028972E-17 ) ) ;
#6338=CARTESIAN_POINT ( 'NONE',  ( 0.1023119647485436629, -0.3500760196667498936, -0.4024809188492812773 ) ) ;
#6347=AXIS2_PLACEMENT_3D ( 'NONE', #6257, #4500, #1014 ) ;
#6367=DIRECTION ( 'NONE',  ( -0.000000000000000000, -0.000000000000000000, 1.000000000000000000 ) ) ;
#6375=DIRECTION ( 'NONE',  ( -1.000000000000000000, 0.000000000000000000, 0.000000000000000000 ) ) ;
#6392=CARTESIAN_POINT ( 'NONE',  ( -0.1922007978147441398, -0.2981786776988376020, -0.4082677165354330340 ) ) ;
#6393=PLANE ( 'NONE',  #5856 ) ;
#6400=CARTESIAN_POINT ( 'NONE',  ( -0.02890955082422807035, 0.3924549231051211451, -0.3862566910637255657 ) ) ;
#6418=ORIENTED_EDGE ( 'NONE', *, *, #4155, .F. ) ;
#6436=ADVANCED_FACE ( 'NONE', ( #19 ), #5332, .T. ) ;
#6440=AXIS2_PLACEMENT_3D ( 'NONE', #6652, #7138, #3047 ) ;
#6446=EDGE_CURVE ( 'NONE', #6705, #5707, #24, .T. ) ;
#6450=CARTESIAN_POINT ( 'NONE',  ( 0.3543307086614173040, -0.03456946083495021638, 4.441920810010739880E-17 ) ) ;
#6455=VERTEX_POINT ( 'NONE', #4758 ) ;
#6488=AXIS2_PLACEMENT_3D ( 'NONE', #1898, #636, #4229 ) ;
#6494=CARTESIAN_POINT ( 'NONE',  ( 0.3543307086614173596, -0.1713008003332313067, -0.02204270589528177851 ) ) ;
#6502=ORIENTED_EDGE ( 'NONE', *, *, #6543, .F. ) ;
#6503=DIRECTION ( 'NONE',  ( -1.000000000000000000, 0.000000000000000000, 0.000000000000000000 ) ) ;
#6504=DIRECTION ( 'NONE',  ( 1.000000000000000000, 0.000000000000000000, 0.000000000000000000 ) ) ;
#6509=ADVANCED_FACE ( 'NONE', ( #3573 ), #1725, .T. ) ;
#6512=CONICAL_SURFACE ( 'NONE', #770, 0.3543307086614173596, 1.047197551196596521 ) ;
#6520=SHAPE_DEFINITION_REPRESENTATION ( #2641, #5265 ) ;
#6529=CYLINDRICAL_SURFACE ( 'NONE', #2706, 0.3543307086614172485 ) ;
#6540=MANIFOLD_SOLID_BREP ( 'TorqueElement', #305 ) ;
#6541=ORIENTED_EDGE ( 'NONE', *, *, #4017, .T. ) ;
#6543=EDGE_CURVE ( 'NONE', #1419, #1683, #1088, .T. ) ;
#6548=DIRECTION ( 'NONE',  ( -0.000000000000000000, -0.000000000000000000, 1.000000000000000000 ) ) ;
#6551=EDGE_CURVE ( 'NONE', #662, #3879, #6727, .T. ) ;
#6553=VERTEX_POINT ( 'NONE', #4914 ) ;
#6558=PRODUCT_DEFINITION_FORMATION_WITH_SPECIFIED_SOURCE ( 'ANY', '', #5321, .NOT_KNOWN. ) ;
#6559=CARTESIAN_POINT ( 'NONE',  ( -0.3253487914207031650, 0.2213056477483777706, -0.3862808132025623009 ) ) ;
#6564=ORIENTED_EDGE ( 'NONE', *, *, #1576, .F. ) ;
#6570=AXIS2_PLACEMENT_3D ( 'NONE', #2898, #6548, #40 ) ;
#6580=DIRECTION ( 'NONE',  ( -0.000000000000000000, -0.000000000000000000, 1.000000000000000000 ) ) ;
#6602=EDGE_CURVE ( 'NONE', #2406, #3362, #4771, .T. ) ;
#6609=CARTESIAN_POINT ( 'NONE',  ( 0.02898191724071416675, 0.3924131423350827874, -0.02198690333287090654 ) ) ;
#6613=CARTESIAN_POINT ( 'NONE',  ( -0.1771653543307088186, -0.3068593950417299876, 7.886165872636028972E-17 ) ) ;
#6641=CARTESIAN_POINT ( 'NONE',  ( 3.414809992080329023E-17, 0.4091458600556405201, -0.3766201741223081378 ) ) ;
#6652=CARTESIAN_POINT ( 'NONE',  ( 0.000000000000000000, 0.000000000000000000, 0.000000000000000000 ) ) ;
#6659=EDGE_LOOP ( 'NONE', ( #4604, #92, #1830, #4530 ) ) ;
#6670=CARTESIAN_POINT ( 'NONE',  ( 0.3543307086614173596, 0.000000000000000000, -0.4082677165354330340 ) ) ;
#6674=CARTESIAN_POINT ( 'NONE',  ( -0.3543307086614173040, -0.06891495372886453918, -0.4052962681128434164 ) ) ;
#6676=B_SPLINE_CURVE_WITH_KNOTS ( 'NONE', 3,
 ( #3698, #5918, #4147, #2468, #1350, #4805 ),
 .UNSPECIFIED., .F., .F.,
 ( 4, 2, 4 ),
 ( 0.01452727543195640389, 0.01715716534226973539, 0.01978705525258306341 ),
 .UNSPECIFIED. ) ;
#6681=CARTESIAN_POINT ( 'NONE',  ( 0.000000000000000000, 0.000000000000000000, 0.000000000000000000 ) ) ;
#6686=CARTESIAN_POINT ( 'NONE',  ( 0.3543307086614173040, 0.2045729300278199825, -0.4082677165354330340 ) ) ;
#6688=CONICAL_SURFACE ( 'NONE', #3017, 0.3543307086614173596, 1.047197551196596521 ) ;
#6691=CARTESIAN_POINT ( 'NONE',  ( 0.2961551751698085488, -0.2381605899494511347, -0.3942397458900141483 ) ) ;
#6694=B_SPLINE_CURVE_WITH_KNOTS ( 'NONE', 3,
 ( #31, #6494, #682, #150, #6450, #1236 ),
 .UNSPECIFIED., .F., .F.,
 ( 4, 2, 4 ),
 ( 0.009270618776430218297, 0.01189894710419331023, 0.01452727543195640389 ),
 .UNSPECIFIED. ) ;
#6695=AXIS2_PLACEMENT_3D ( 'NONE', #7515, #7109, #1868 ) ;
#6700=VECTOR ( 'NONE', #2535, 39.37007874015748143 ) ;
#6705=VERTEX_POINT ( 'NONE', #4991 ) ;
#6715=AXIS2_PLACEMENT_3D ( 'NONE', #2635, #7359, #3532 ) ;
#6727=CIRCLE ( 'NONE', #2694, 0.3543307086614173596 ) ;
#6732=EDGE_CURVE ( 'NONE', #3999, #5611, #2573, .T. ) ;
#6747=VECTOR ( 'NONE', #3225, 39.37007874015748143 ) ;
#6748=ORIENTED_EDGE ( 'NONE', *, *, #6957, .T. ) ;
#6757=B_SPLINE_CURVE_WITH_KNOTS ( 'NONE', 3,
 ( #3921, #6392, #5692, #1137, #449, #4567, #2731, #5186 ),
 .UNSPECIFIED., .F., .F.,
 ( 4, 2, 2, 4 ),
 ( 0.005257893453559908843, 0.006567392922673239916, 0.007876892391786570122, 0.01049589133001323227 ),
 .UNSPECIFIED. ) ;
#6760=FACE_BOUND ( 'NONE', #1253, .T. ) ;
#6777=EDGE_LOOP ( 'NONE', ( #2188, #3130, #199, #819, #3067, #80 ) ) ;
#6786=ORIENTED_EDGE ( 'NONE', *, *, #148, .F. ) ;
#6793=DIRECTION ( 'NONE',  ( 0.5000000000000006661, 0.8660254037844382635, -0.000000000000000000 ) ) ;
#6800=DIRECTION ( 'NONE',  ( -1.000000000000000000, 0.000000000000000000, 0.000000000000000000 ) ) ;
#6801=DIRECTION ( 'NONE',  ( -1.000000000000000000, 0.000000000000000000, 0.000000000000000000 ) ) ;
#6811=CIRCLE ( 'NONE', #6570, 0.3543307086614172485 ) ;
#6860=CARTESIAN_POINT ( 'NONE',  ( 0.000000000000000000, 0.000000000000000000, 0.1188976377952756375 ) ) ;
#6868=ADVANCED_FACE ( 'NONE', ( #691 ), #2450, .T. ) ;
#6877=LINE ( 'NONE', #1628, #7186 ) ;
#6889=ORIENTED_EDGE ( 'NONE', *, *, #979, .F. ) ;
#6909=DIRECTION ( 'NONE',  ( -0.000000000000000000, -0.000000000000000000, 1.000000000000000000 ) ) ;
#6911=CARTESIAN_POINT ( 'NONE',  ( 0.000000000000000000, 0.000000000000000000, -0.4082677165354330340 ) ) ;
#6915=CARTESIAN_POINT ( 'NONE',  ( 0.2073036836782039261, 0.2894590224800283051, -0.4075196867561207692 ) ) ;
#6917=EDGE_CURVE ( 'NONE', #3331, #1068, #621, .T. ) ;
#6926=EDGE_CURVE ( 'NONE', #4931, #2266, #1173, .T. ) ;
#6927=DIRECTION ( 'NONE',  ( 0.000000000000000000, 0.000000000000000000, -1.000000000000000000 ) ) ;
#6934=VECTOR ( 'NONE', #1786, 39.37007874015748143 ) ;
#6944=CARTESIAN_POINT ( 'NONE',  ( -1.126887297386508504E-15, -0.4091458600556405756, -0.3766201741223081378 ) ) ;
#6949=CONICAL_SURFACE ( 'NONE', #601, 0.3543307086614173596, 1.047197551196596521 ) ;
#6954=CARTESIAN_POINT ( 'NONE',  ( -0.2699662542182227343, 3.306133091061471023E-17, 0.3732633159281743551 ) ) ;
#6957=EDGE_CURVE ( 'NONE', #3631, #4410, #3095, .T. ) ;
#6960=CARTESIAN_POINT ( 'NONE',  ( 0.000000000000000000, 0.000000000000000000, -0.3865922971001068409 ) ) ;
#6963=ORIENTED_EDGE ( 'NONE', *, *, #3941, .F. ) ;
#6966=EDGE_CURVE ( 'NONE', #662, #1000, #6676, .T. ) ;
#6990=CARTESIAN_POINT ( 'NONE',  ( 0.000000000000000000, 0.000000000000000000, 0.000000000000000000 ) ) ;
#6993=ORIENTED_EDGE ( 'NONE', *, *, #851, .T. ) ;
#7005=EDGE_CURVE ( 'NONE', #1762, #5183, #5525, .T. ) ;
#7007=DIRECTION ( 'NONE',  ( 0.000000000000000000, 0.000000000000000000, 1.000000000000000000 ) ) ;
#7038=DIRECTION ( 'NONE',  ( -1.000000000000000000, 0.000000000000000000, 0.000000000000000000 ) ) ;
#7049=ORIENTED_EDGE ( 'NONE', *, *, #1596, .F. ) ;
#7055=AXIS2_PLACEMENT_3D ( 'NONE', #4199, #153, #1278 ) ;
#7069=CIRCLE ( 'NONE', #4142, 0.3543307086614173596 ) ;
#7080=DIRECTION ( 'NONE',  ( 1.000000000000000000, 0.000000000000000000, 0.000000000000000000 ) ) ;
#7088=DIRECTION ( 'NONE',  ( 1.000000000000000000, 0.000000000000000000, 0.000000000000000000 ) ) ;
#7109=DIRECTION ( 'NONE',  ( 0.000000000000000000, 0.000000000000000000, -1.000000000000000000 ) ) ;
#7118=CARTESIAN_POINT ( 'NONE',  ( -0.1771653543307089018, -0.3068593950417300986, -0.4082677165354330340 ) ) ;
#7121=ORIENTED_EDGE ( 'NONE', *, *, #148, .T. ) ;
#7123=EDGE_LOOP ( 'NONE', ( #7422, #273, #348 ) ) ;
#7126=ORIENTED_EDGE ( 'NONE', *, *, #6184, .F. ) ;
#7138=DIRECTION ( 'NONE',  ( -0.000000000000000000, 0.000000000000000000, -1.000000000000000000 ) ) ;
#7139=CARTESIAN_POINT ( 'NONE',  ( 6.901988839087968355E-18, 0.4091458600556405201, -0.4082677165354330340 ) ) ;
#7144=ADVANCED_FACE ( 'NONE', ( #5201, #3364 ), #5674, .F. ) ;
#7149=ORIENTED_EDGE ( 'NONE', *, *, #6732, .F. ) ;
#7152=EDGE_CURVE ( 'NONE', #5611, #929, #5683, .T. ) ;
#7167=CARTESIAN_POINT ( 'NONE',  ( 0.02898191724071414593, 0.3924131423350827874, -0.3862808132025621344 ) ) ;
#7175=CARTESIAN_POINT ( 'NONE',  ( -0.3543307086614173040, 0.2045729300278199547, -0.4082677165354330340 ) ) ;
#7182=CARTESIAN_POINT ( 'NONE',  ( -9.561467977824920278E-16, -0.4091458600556405756, -0.03164754241312491001 ) ) ;
#7186=VECTOR ( 'NONE', #5739, 39.37007874015748143 ) ;
#7201=CARTESIAN_POINT ( 'NONE',  ( 0.000000000000000000, 0.000000000000000000, 0.3732633159281743551 ) ) ;
#7214=EDGE_LOOP ( 'NONE', ( #1432, #4835, #7121, #4262, #7049, #5722 ) ) ;
#7225=AXIS2_PLACEMENT_3D ( 'NONE', #3342, #2763, #5790 ) ;
#7226=DIRECTION ( 'NONE',  ( 1.000000000000000000, 0.000000000000000000, 0.000000000000000000 ) ) ;
#7233=CARTESIAN_POINT ( 'NONE',  ( 0.1771653543307088463, -0.3068593950417300431, 7.886165872636028972E-17 ) ) ;
#7239=CONICAL_SURFACE ( 'NONE', #2825, 0.3543307086614173596, 1.047197551196596521 ) ;
#7242=EDGE_LOOP ( 'NONE', ( #4902, #1710, #238 ) ) ;
#7283=EDGE_CURVE ( 'NONE', #1378, #6705, #5881, .T. ) ;
#7286=VERTEX_POINT ( 'NONE', #4650 ) ;
#7291=CARTESIAN_POINT ( 'NONE',  ( -0.1771653543307089573, 0.3068593950417301541, 0.000000000000000000 ) ) ;
#7306=CARTESIAN_POINT ( 'NONE',  ( -0.1171731013849884873, -0.3414959384292345357, -0.003016182236739476611 ) ) ;
#7319=CIRCLE ( 'NONE', #2087, 0.2948818897637794922 ) ;
#7321=DIRECTION ( 'NONE',  ( 0.000000000000000000, 0.000000000000000000, -1.000000000000000000 ) ) ;
#7333=CARTESIAN_POINT ( 'NONE',  ( 0.2962704110120346068, 0.2380940585049209079, -0.01405589313879318687 ) ) ;
#7339=ORIENTED_EDGE ( 'NONE', *, *, #6543, .T. ) ;
#7343=STYLED_ITEM('',(#7587),#6540);
#7345=CARTESIAN_POINT ( 'NONE',  ( 0.2371576072764298437, -0.2722228516542264942, -0.003016182236739480948 ) ) ;
#7359=DIRECTION ( 'NONE',  ( -0.000000000000000000, -0.000000000000000000, 1.000000000000000000 ) ) ;
#7372=CARTESIAN_POINT ( 'NONE',  ( 0.1771653543307089296, -0.3068593950417301541, -0.4082677165354330340 ) ) ;
#7386=B_SPLINE_CURVE_WITH_KNOTS ( 'NONE', 3,
 ( #2574, #4911, #1416, #6674, #3802, #405 ),
 .UNSPECIFIED., .F., .F.,
 ( 4, 2, 4 ),
 ( 0.009270618776430216562, 0.01189894710419331023, 0.01452727543195640389 ),
 .UNSPECIFIED. ) ;
#7407=CARTESIAN_POINT ( 'NONE',  ( 0.2520187439128737106, 0.2636427704167111918, -0.4024809188492816658 ) ) ;
#7409=CARTESIAN_POINT ( 'NONE',  ( -0.3543307086614173040, -0.2045729300278205653, -0.4082677165354330340 ) ) ;
#7422=ORIENTED_EDGE ( 'NONE', *, *, #7152, .T. ) ;
#7436=AXIS2_PLACEMENT_3D ( 'NONE', #4273, #5390, #2549 ) ;
#7441=AXIS2_PLACEMENT_3D ( 'NONE', #4235, #5926, #2393 ) ;
#7444=CARTESIAN_POINT ( 'NONE',  ( 0.1771653543307089296, 0.3068593950417301541, -0.4082677165354330340 ) ) ;
#7448=CYLINDRICAL_SURFACE ( 'NONE', #889, 0.2066929133858267931 ) ;
#7451=AXIS2_PLACEMENT_3D ( 'NONE', #4299, #3732, #4342 ) ;
#7464=PLANE ( 'NONE',  #669 ) ;
#7479=ADVANCED_FACE ( 'NONE', ( #226, #4843 ), #6003, .F. ) ;
#7482=CARTESIAN_POINT ( 'NONE',  ( 0.2962704110120346623, 0.2380940585049209357, -0.3942118233966399599 ) ) ;
#7485=ORIENTED_EDGE ( 'NONE', *, *, #4860, .T. ) ;
#7499=DIRECTION ( 'NONE',  ( -0.000000000000000000, -0.000000000000000000, 1.000000000000000000 ) ) ;
#7502=CARTESIAN_POINT ( 'NONE',  ( -0.1023119647485438433, 0.3500760196667492274, -0.4024809188492814993 ) ) ;
#7503=( LENGTH_UNIT ( ) NAMED_UNIT ( * ) SI_UNIT ( $, .METRE. ) );
#7515=CARTESIAN_POINT ( 'NONE',  ( 0.000000000000000000, 0.000000000000000000, 0.000000000000000000 ) ) ;
#7581=COLOUR_RGB('Black',0.12,0.14,0.17);
#7582=FILL_AREA_STYLE_COLOUR('',#7581);
#7583=FILL_AREA_STYLE('',(#7582));
#7584=SURFACE_STYLE_FILL_AREA(#7583);
#7585=SURFACE_SIDE_STYLE('',(#7584));
#7586=SURFACE_STYLE_USAGE(.BOTH.,#7585);
#7587=PRESENTATION_STYLE_ASSIGNMENT((#7586));
ENDSEC;
END-ISO-10303-21;
